ISO-10303-21;
HEADER;
FILE_DESCRIPTION (('STEP AP214'),
    '1' );
FILE_NAME ('circlip for shafts normal_din_Circlip DIN 471 - 7 x 0.8.step',
    '2026-10-26T05:17:54',
    ( '' ),
    ( '' ),
    'SwSTEP 2.0',
    'SolidWorks 2026',
    '' );
FILE_SCHEMA (( 'AUTOMOTIVE_DESIGN' ));
ENDSEC;

DATA;
#7=ADVANCED_FACE ( 'NONE', ( #12422 ), #11435, .F. ) ;
#15=ORIENTED_EDGE ( 'NONE', *, *, #11202, .T. ) ;
#31=( NAMED_UNIT ( * ) SI_UNIT ( $, .STERADIAN. ) SOLID_ANGLE_UNIT ( ) );
#72=CARTESIAN_POINT ( 'NONE',  ( -1.000000000000000000, -4.873461295629625489, -0.8000000000000000444 ) ) ;
#74=DIRECTION ( 'NONE',  ( 0.000000000000000000, 0.000000000000000000, 1.000000000000000000 ) ) ;
#85=VERTEX_POINT ( 'NONE', #9987 ) ;
#86=VECTOR ( 'NONE', #8647, 1000.000000000000000 ) ;
#106=DIRECTION ( 'NONE',  ( 0.000000000000000000, 0.000000000000000000, 1.000000000000000000 ) ) ;
#110=ORIENTED_EDGE ( 'NONE', *, *, #11359, .T. ) ;
#140=CARTESIAN_POINT ( 'NONE',  ( -1.000000000000000000, -5.473461295629626022, -0.8000000000000000444 ) ) ;
#146=DIRECTION ( 'NONE',  ( 1.000000000000000000, 0.000000000000000000, 0.000000000000000000 ) ) ;
#169=VERTEX_POINT ( 'NONE', #6912 ) ;
#204=LINE ( 'NONE', #1265, #6022 ) ;
#209=DIRECTION ( 'NONE',  ( 0.000000000000000000, 0.000000000000000000, 1.000000000000000000 ) ) ;
#213=ORIENTED_EDGE ( 'NONE', *, *, #1279, .T. ) ;
#214=EDGE_CURVE ( 'NONE', #1472, #1154, #10317, .T. ) ;
#227=ORIENTED_EDGE ( 'NONE', *, *, #6357, .F. ) ;
#281=CIRCLE ( 'NONE', #7814, 4.338286831716297698 ) ;
#290=AXIS2_PLACEMENT_3D ( 'NONE', #12563, #2683, #9478 ) ;
#318=DIRECTION ( 'NONE',  ( 0.000000000000000000, 0.000000000000000000, 1.000000000000000000 ) ) ;
#323=ORIENTED_EDGE ( 'NONE', *, *, #9643, .F. ) ;
#359=ORIENTED_EDGE ( 'NONE', *, *, #812, .T. ) ;
#362=VERTEX_POINT ( 'NONE', #4108 ) ;
#397=CARTESIAN_POINT ( 'NONE',  ( 0.000000000000000000, 0.000000000000000000, -0.8000000000000000444 ) ) ;
#398=LINE ( 'NONE', #10557, #7920 ) ;
#433=ORIENTED_EDGE ( 'NONE', *, *, #4981, .F. ) ;
#478=ORIENTED_EDGE ( 'NONE', *, *, #11274, .T. ) ;
#509=CARTESIAN_POINT ( 'NONE',  ( -2.387319993259524598, -4.036502139894371233, 0.000000000000000000 ) ) ;
#515=CARTESIAN_POINT ( 'NONE',  ( -3.068288344391240763, -2.655262421758692426, -0.8000000000000000444 ) ) ;
#546=ORIENTED_EDGE ( 'NONE', *, *, #10576, .T. ) ;
#555=CARTESIAN_POINT ( 'NONE',  ( 0.1038759689922479496, -3.348389132562988646, -0.8000000000000000444 ) ) ;
#560=ORIENTED_EDGE ( 'NONE', *, *, #12372, .T. ) ;
#589=VECTOR ( 'NONE', #11996, 1000.000000000000000 ) ;
#599=DIRECTION ( 'NONE',  ( 1.000000000000000000, 0.000000000000000000, 0.000000000000000000 ) ) ;
#617=DIRECTION ( 'NONE',  ( 1.000000000000000000, 0.000000000000000000, 0.000000000000000000 ) ) ;
#634=CIRCLE ( 'NONE', #12768, 3.350000000000000089 ) ;
#710=ORIENTED_EDGE ( 'NONE', *, *, #10661, .T. ) ;
#715=ADVANCED_FACE ( 'NONE', ( #10234 ), #11079, .T. ) ;
#717=DIRECTION ( 'NONE',  ( 0.000000000000000000, 0.000000000000000000, 1.000000000000000000 ) ) ;
#765=ORIENTED_EDGE ( 'NONE', *, *, #4326, .T. ) ;
#780=CARTESIAN_POINT ( 'NONE',  ( 4.763019983628629994, -4.349268977144817860, 0.000000000000000000 ) ) ;
#812=EDGE_CURVE ( 'NONE', #6247, #5477, #281, .T. ) ;
#817=CIRCLE ( 'NONE', #12527, 2.396199811936269963 ) ;
#830=CARTESIAN_POINT ( 'NONE',  ( -0.1325741768533960641, -4.273461295629625845, 0.000000000000000000 ) ) ;
#853=AXIS2_PLACEMENT_3D ( 'NONE', #3691, #4729, #3625 ) ;
#863=PLANE ( 'NONE',  #9839 ) ;
#870=VERTEX_POINT ( 'NONE', #2582 ) ;
#881=ORIENTED_EDGE ( 'NONE', *, *, #2430, .T. ) ;
#883=ADVANCED_FACE ( 'NONE', ( #10491 ), #5650, .F. ) ;
#891=ORIENTED_EDGE ( 'NONE', *, *, #5454, .T. ) ;
#893=FACE_OUTER_BOUND ( 'NONE', #5421, .T. ) ;
#912=LINE ( 'NONE', #11787, #8517 ) ;
#963=VECTOR ( 'NONE', #2574, 1000.000000000000000 ) ;
#973=DIRECTION ( 'NONE',  ( 0.000000000000000000, 0.000000000000000000, 1.000000000000000000 ) ) ;
#986=DIRECTION ( 'NONE',  ( 1.000000000000000000, -0.000000000000000000, -0.000000000000000000 ) ) ;
#988=EDGE_CURVE ( 'NONE', #4325, #9537, #6991, .T. ) ;
#990=DIRECTION ( 'NONE',  ( -0.000000000000000000, -0.000000000000000000, -1.000000000000000000 ) ) ;
#995=EDGE_LOOP ( 'NONE', ( #11036, #8835, #1603, #7933 ) ) ;
#1010=CARTESIAN_POINT ( 'NONE',  ( 0.1325741768533959530, -4.273461295629625845, -0.8000000000000000444 ) ) ;
#1011=ORIENTED_EDGE ( 'NONE', *, *, #12514, .F. ) ;
#1024=SURFACE_SIDE_STYLE ('',( #11096 ) ) ;
#1039=ORIENTED_EDGE ( 'NONE', *, *, #1444, .F. ) ;
#1058=CARTESIAN_POINT ( 'NONE',  ( 1.000000000000000000, -5.473461295629626022, 0.000000000000000000 ) ) ;
#1067=ADVANCED_FACE ( 'NONE', ( #8724 ), #5714, .F. ) ;
#1069=DIRECTION ( 'NONE',  ( 1.000000000000000000, 0.000000000000000000, 0.000000000000000000 ) ) ;
#1084=CARTESIAN_POINT ( 'NONE',  ( 1.000000000000000000, -4.873461295629625489, -0.8000000000000000444 ) ) ;
#1086=ORIENTED_EDGE ( 'NONE', *, *, #10661, .F. ) ;
#1097=ORIENTED_EDGE ( 'NONE', *, *, #1307, .F. ) ;
#1100=EDGE_CURVE ( 'NONE', #8436, #7369, #1983, .T. ) ;
#1103=ADVANCED_FACE ( 'NONE', ( #9105 ), #8133, .T. ) ;
#1107=( GEOMETRIC_REPRESENTATION_CONTEXT ( 3 ) GLOBAL_UNCERTAINTY_ASSIGNED_CONTEXT ( ( #7087 ) ) GLOBAL_UNIT_ASSIGNED_CONTEXT ( ( #1952, #9928, #1155 ) ) REPRESENTATION_CONTEXT ( 'NONE', 'WORKASPACE' ) );
#1110=DIRECTION ( 'NONE',  ( 1.000000000000000000, 0.000000000000000000, 0.000000000000000000 ) ) ;
#1111=CLOSED_SHELL ( 'NONE', ( #7998, #1318, #11759, #3374, #1067, #11979, #11060, #2711, #2077, #5346, #1103, #6314, #5407, #715, #7473, #6396, #5272, #6442, #10240, #7, #8396, #2560, #4373, #883, #6299, #12362, #3318 ) ) ;
#1129=CARTESIAN_POINT ( 'NONE',  ( -2.387319993259524598, -4.036502139894371233, -0.8000000000000000444 ) ) ;
#1140=VERTEX_POINT ( 'NONE', #7386 ) ;
#1151=CARTESIAN_POINT ( 'NONE',  ( 3.350000000000000089, 0.000000000000000000, -0.8000000000000000444 ) ) ;
#1154=VERTEX_POINT ( 'NONE', #11439 ) ;
#1155=( NAMED_UNIT ( * ) SI_UNIT ( $, .STERADIAN. ) SOLID_ANGLE_UNIT ( ) );
#1193=UNCERTAINTY_MEASURE_WITH_UNIT (LENGTH_MEASURE( 1.000000000000000082E-05 ), #9138, 'distance_accuracy_value', 'NONE');
#1198=EDGE_CURVE ( 'NONE', #9926, #4325, #8868, .T. ) ;
#1209=VERTEX_POINT ( 'NONE', #4643 ) ;
#1237=ORIENTED_EDGE ( 'NONE', *, *, #9652, .F. ) ;
#1258=CARTESIAN_POINT ( 'NONE',  ( 1.000000000000000000, -4.873461295629625489, -0.8000000000000000444 ) ) ;
#1260=CARTESIAN_POINT ( 'NONE',  ( -3.068288344391240763, -2.655262421758692426, 0.000000000000000000 ) ) ;
#1265=CARTESIAN_POINT ( 'NONE',  ( 1.000000000000000000, -5.473461295629626022, 0.000000000000000000 ) ) ;
#1266=CIRCLE ( 'NONE', #5015, 0.7499999999999997780 ) ;
#1279=EDGE_CURVE ( 'NONE', #7668, #8436, #12840, .T. ) ;
#1290=ORIENTED_EDGE ( 'NONE', *, *, #5724, .F. ) ;
#1303=ORIENTED_EDGE ( 'NONE', *, *, #1642, .T. ) ;
#1304=DIRECTION ( 'NONE',  ( 0.03100775193798453039, 0.9995191440486532741, -0.000000000000000000 ) ) ;
#1307=EDGE_CURVE ( 'NONE', #2471, #5455, #12751, .T. ) ;
#1318=ADVANCED_FACE ( 'NONE', ( #7771 ), #1564, .T. ) ;
#1341=AXIS2_PLACEMENT_3D ( 'NONE', #7691, #5529, #617 ) ;
#1377=DIRECTION ( 'NONE',  ( 0.000000000000000000, 0.000000000000000000, 1.000000000000000000 ) ) ;
#1389=AXIS2_PLACEMENT_3D ( 'NONE', #11217, #11017, #146 ) ;
#1410=FACE_OUTER_BOUND ( 'NONE', #10954, .T. ) ;
#1444=EDGE_CURVE ( 'NONE', #6695, #870, #3876, .T. ) ;
#1447=LINE ( 'NONE', #9429, #12008 ) ;
#1459=CARTESIAN_POINT ( 'NONE',  ( 2.387319993259524598, -4.036502139894371233, -0.8000000000000000444 ) ) ;
#1472=VERTEX_POINT ( 'NONE', #11949 ) ;
#1479=VERTEX_POINT ( 'NONE', #830 ) ;
#1507=CARTESIAN_POINT ( 'NONE',  ( -0.1698013801012111523, -5.473461295629626022, -0.8000000000000000444 ) ) ;
#1508=AXIS2_PLACEMENT_3D ( 'NONE', #6409, #318, #11191 ) ;
#1522=DIRECTION ( 'NONE',  ( 0.9914448613738103822, -0.1305261922200528224, 0.000000000000000000 ) ) ;
#1545=DIRECTION ( 'NONE',  ( -0.9995191440486532741, -0.03100775193798452692, 0.000000000000000000 ) ) ;
#1548=AXIS2_PLACEMENT_3D ( 'NONE', #4416, #6432, #8603 ) ;
#1556=EDGE_LOOP ( 'NONE', ( #12315, #4021, #891, #11187 ) ) ;
#1558=AXIS2_PLACEMENT_3D ( 'NONE', #12626, #10527, #2748 ) ;
#1564=CYLINDRICAL_SURFACE ( 'NONE', #12216, 4.338286831716297698 ) ;
#1569=VERTEX_POINT ( 'NONE', #12346 ) ;
#1586=DIRECTION ( 'NONE',  ( -1.000000000000000000, -0.000000000000000000, -0.000000000000000000 ) ) ;
#1596=CYLINDRICAL_SURFACE ( 'NONE', #10760, 0.5999999999999998668 ) ;
#1603=ORIENTED_EDGE ( 'NONE', *, *, #10158, .T. ) ;
#1619=ORIENTED_EDGE ( 'NONE', *, *, #12524, .T. ) ;
#1642=EDGE_CURVE ( 'NONE', #8436, #4325, #12217, .T. ) ;
#1650=EDGE_LOOP ( 'NONE', ( #2698, #765, #9307, #3005 ) ) ;
#1652=CARTESIAN_POINT ( 'NONE',  ( -0.9999999999999997780, -4.273461295629625845, -0.8000000000000000444 ) ) ;
#1657=FACE_OUTER_BOUND ( 'NONE', #4454, .T. ) ;
#1678=EDGE_LOOP ( 'NONE', ( #10019, #12881, #6928, #12253 ) ) ;
#1703=LINE ( 'NONE', #3735, #2331 ) ;
#1704=ORIENTED_EDGE ( 'NONE', *, *, #2054, .F. ) ;
#1710=EDGE_CURVE ( 'NONE', #9206, #3826, #8877, .T. ) ;
#1713=EDGE_LOOP ( 'NONE', ( #9085, #4380, #10994, #12223 ) ) ;
#1716=ORIENTED_EDGE ( 'NONE', *, *, #988, .T. ) ;
#1734=DIRECTION ( 'NONE',  ( 0.1305261922200528224, -0.9914448613738103822, 0.000000000000000000 ) ) ;
#1744=VERTEX_POINT ( 'NONE', #9459 ) ;
#1760=CARTESIAN_POINT ( 'NONE',  ( -0.1698013801012111523, -5.473461295629626022, -0.8000000000000000444 ) ) ;
#1776=AXIS2_PLACEMENT_3D ( 'NONE', #10333, #3167, #2182 ) ;
#1781=DIRECTION ( 'NONE',  ( 1.000000000000000000, 0.000000000000000000, 0.000000000000000000 ) ) ;
#1795=VECTOR ( 'NONE', #209, 1000.000000000000000 ) ;
#1854=CARTESIAN_POINT ( 'NONE',  ( 1.000000000000000000, -5.473461295629626022, -0.8000000000000000444 ) ) ;
#1892=VERTEX_POINT ( 'NONE', #2065 ) ;
#1895=CARTESIAN_POINT ( 'NONE',  ( -0.2000000000000000111, -6.446898479113814417, -0.8000000000000000444 ) ) ;
#1901=CARTESIAN_POINT ( 'NONE',  ( 1.000000000000000000, -5.473461295629626022, -0.8000000000000000444 ) ) ;
#1921=ORIENTED_EDGE ( 'NONE', *, *, #8275, .F. ) ;
#1930=STYLED_ITEM('',(#13002),#12156);
#1939=VERTEX_POINT ( 'NONE', #11814 ) ;
#1952=( LENGTH_UNIT ( ) NAMED_UNIT ( * ) SI_UNIT ( .MILLI., .METRE. ) );
#1958=DIRECTION ( 'NONE',  ( 1.000000000000000000, 0.000000000000000000, 0.000000000000000000 ) ) ;
#1983=CIRCLE ( 'NONE', #8671, 3.350000000000000089 ) ;
#1987=VECTOR ( 'NONE', #986, 1000.000000000000000 ) ;
#2020=DIRECTION ( 'NONE',  ( 0.000000000000000000, -0.000000000000000000, 1.000000000000000000 ) ) ;
#2036=FACE_OUTER_BOUND ( 'NONE', #995, .T. ) ;
#2042=( LENGTH_UNIT ( ) NAMED_UNIT ( * ) SI_UNIT ( .MILLI., .METRE. ) );
#2054=EDGE_CURVE ( 'NONE', #1154, #3826, #4160, .T. ) ;
#2065=CARTESIAN_POINT ( 'NONE',  ( 0.1999999999999965694, -6.446898479113814417, -0.8000000000000000444 ) ) ;
#2071=LINE ( 'NONE', #2866, #9761 ) ;
#2077=ADVANCED_FACE ( 'NONE', ( #3184 ), #10297, .T. ) ;
#2087=ORIENTED_EDGE ( 'NONE', *, *, #7886, .F. ) ;
#2114=EDGE_CURVE ( 'NONE', #1140, #5477, #2200, .T. ) ;
#2119=ORIENTED_EDGE ( 'NONE', *, *, #214, .T. ) ;
#2150=PRESENTATION_STYLE_ASSIGNMENT (( #3001 ) ) ;
#2165=LINE ( 'NONE', #9155, #2496 ) ;
#2166=EDGE_CURVE ( 'NONE', #9809, #169, #7487, .T. ) ;
#2169=COLOUR_RGB ( '',1.000000000000000000, 0.9490196078431372140, 0.9098039215686274384 ) ;
#2173=( NAMED_UNIT ( * ) SI_UNIT ( $, .STERADIAN. ) SOLID_ANGLE_UNIT ( ) );
#2182=DIRECTION ( 'NONE',  ( 1.000000000000000000, 0.000000000000000000, 0.000000000000000000 ) ) ;
#2200=LINE ( 'NONE', #6178, #1795 ) ;
#2220=FILL_AREA_STYLE ('',( #12221 ) ) ;
#2224=PLANE ( 'NONE',  #11311 ) ;
#2227=AXIS2_PLACEMENT_3D ( 'NONE', #12883, #8886, #5813 ) ;
#2252=CARTESIAN_POINT ( 'NONE',  ( -4.763019983628629994, -4.349268977144818749, -0.8000000000000000444 ) ) ;
#2306=DIRECTION ( 'NONE',  ( 0.000000000000000000, 0.000000000000000000, 1.000000000000000000 ) ) ;
#2331=VECTOR ( 'NONE', #10659, 1000.000000000000000 ) ;
#2338=ORIENTED_EDGE ( 'NONE', *, *, #1198, .T. ) ;
#2368=CIRCLE ( 'NONE', #7365, 3.350000000000000089 ) ;
#2384=CARTESIAN_POINT ( 'NONE',  ( 1.436050757534458100, -5.516136167806656943, -0.8000000000000000444 ) ) ;
#2385=FACE_OUTER_BOUND ( 'NONE', #7262, .T. ) ;
#2401=VECTOR ( 'NONE', #6897, 1000.000000000000000 ) ;
#2402=CARTESIAN_POINT ( 'NONE',  ( 2.387319993259524598, -4.036502139894371233, -0.8000000000000000444 ) ) ;
#2430=EDGE_CURVE ( 'NONE', #7384, #7875, #11194, .T. ) ;
#2439=ORIENTED_EDGE ( 'NONE', *, *, #6829, .T. ) ;
#2471=VERTEX_POINT ( 'NONE', #5182 ) ;
#2482=LINE ( 'NONE', #4701, #10293 ) ;
#2496=VECTOR ( 'NONE', #1304, 1000.000000000000114 ) ;
#2516=FACE_OUTER_BOUND ( 'NONE', #10675, .T. ) ;
#2529=DIRECTION ( 'NONE',  ( 1.000000000000000000, 0.000000000000000000, 0.000000000000000000 ) ) ;
#2560=ADVANCED_FACE ( 'NONE', ( #6162 ), #7343, .F. ) ;
#2570=ORIENTED_EDGE ( 'NONE', *, *, #4635, .F. ) ;
#2574=DIRECTION ( 'NONE',  ( -0.000000000000000000, -0.000000000000000000, 1.000000000000000000 ) ) ;
#2582=CARTESIAN_POINT ( 'NONE',  ( 1.599999999999999867, -4.873461295629625489, -0.8000000000000000444 ) ) ;
#2593=AXIS2_PLACEMENT_3D ( 'NONE', #4042, #8031, #7044 ) ;
#2596=CARTESIAN_POINT ( 'NONE',  ( 1.625004804578465745, -6.241943558307532669, 0.000000000000000000 ) ) ;
#2645=CYLINDRICAL_SURFACE ( 'NONE', #11019, 0.7500000000000000000 ) ;
#2655=VECTOR ( 'NONE', #11610, 1000.000000000000000 ) ;
#2683=DIRECTION ( 'NONE',  ( -0.000000000000000000, -0.000000000000000000, -1.000000000000000000 ) ) ;
#2690=ORIENTED_EDGE ( 'NONE', *, *, #5106, .F. ) ;
#2698=ORIENTED_EDGE ( 'NONE', *, *, #7886, .T. ) ;
#2700=ORIENTED_EDGE ( 'NONE', *, *, #10576, .F. ) ;
#2702=AXIS2_PLACEMENT_3D ( 'NONE', #6364, #3178, #7225 ) ;
#2711=ADVANCED_FACE ( 'NONE', ( #2036 ), #5165, .F. ) ;
#2748=DIRECTION ( 'NONE',  ( 1.000000000000000000, 0.000000000000000000, 0.000000000000000000 ) ) ;
#2761=DIRECTION ( 'NONE',  ( 1.000000000000000000, 0.000000000000000000, -0.000000000000000000 ) ) ;
#2764=CARTESIAN_POINT ( 'NONE',  ( 4.763019983628629994, -4.349268977144817860, -0.8000000000000000444 ) ) ;
#2771=LINE ( 'NONE', #6744, #11214 ) ;
#2811=DIRECTION ( 'NONE',  ( 0.000000000000000000, 0.000000000000000000, 1.000000000000000000 ) ) ;
#2854=CARTESIAN_POINT ( 'NONE',  ( 0.000000000000000000, 0.000000000000000000, -0.8000000000000000444 ) ) ;
#2866=CARTESIAN_POINT ( 'NONE',  ( 2.387319993259524598, -4.036502139894371233, 0.000000000000000000 ) ) ;
#2875=ORIENTED_EDGE ( 'NONE', *, *, #1710, .F. ) ;
#2891=LINE ( 'NONE', #1901, #5631 ) ;
#2923=LINE ( 'NONE', #4944, #12758 ) ;
#2947=LINE ( 'NONE', #12819, #7492 ) ;
#2954=VECTOR ( 'NONE', #6822, 1000.000000000000000 ) ;
#2963=LINE ( 'NONE', #3695, #8345 ) ;
#2983=CARTESIAN_POINT ( 'NONE',  ( 4.338286831716297698, 0.4117131682837005258, -0.8000000000000000444 ) ) ;
#2984=CARTESIAN_POINT ( 'NONE',  ( -1.000000000000000000, -5.473461295629626022, -0.8000000000000000444 ) ) ;
#3001=SURFACE_STYLE_USAGE ( .BOTH. , #1024 ) ;
#3005=ORIENTED_EDGE ( 'NONE', *, *, #8313, .F. ) ;
#3036=LINE ( 'NONE', #9043, #11717 ) ;
#3043=CARTESIAN_POINT ( 'NONE',  ( 0.000000000000000000, 0.000000000000000000, 0.000000000000000000 ) ) ;
#3056=EDGE_CURVE ( 'NONE', #870, #6548, #12862, .T. ) ;
#3112=DIRECTION ( 'NONE',  ( 0.1305261922200528224, -0.9914448613738103822, 0.000000000000000000 ) ) ;
#3122=ORIENTED_EDGE ( 'NONE', *, *, #5106, .T. ) ;
#3167=DIRECTION ( 'NONE',  ( 0.000000000000000000, 0.000000000000000000, 1.000000000000000000 ) ) ;
#3177=DIRECTION ( 'NONE',  ( 1.000000000000000000, 0.000000000000000000, 0.000000000000000000 ) ) ;
#3178=DIRECTION ( 'NONE',  ( 0.000000000000000000, -1.000000000000000000, -0.000000000000000000 ) ) ;
#3183=APPLICATION_CONTEXT ( 'automotive_design' ) ;
#3184=FACE_OUTER_BOUND ( 'NONE', #9806, .T. ) ;
#3200=VECTOR ( 'NONE', #10123, 1000.000000000000000 ) ;
#3212=ORIENTED_EDGE ( 'NONE', *, *, #3298, .F. ) ;
#3223=DIRECTION ( 'NONE',  ( 0.000000000000000000, 0.000000000000000000, -1.000000000000000000 ) ) ;
#3247=VECTOR ( 'NONE', #11468, 1000.000000000000114 ) ;
#3265=VECTOR ( 'NONE', #12500, 1000.000000000000000 ) ;
#3280=VERTEX_POINT ( 'NONE', #509 ) ;
#3293=AXIS2_PLACEMENT_3D ( 'NONE', #9096, #10705, #3658 ) ;
#3294=DIRECTION ( 'NONE',  ( 1.000000000000000000, 0.000000000000000000, 0.000000000000000000 ) ) ;
#3298=EDGE_CURVE ( 'NONE', #8873, #5463, #10657, .T. ) ;
#3315=DIRECTION ( 'NONE',  ( 0.000000000000000000, 0.000000000000000000, 1.000000000000000000 ) ) ;
#3318=ADVANCED_FACE ( 'NONE', ( #893 ), #5748, .F. ) ;
#3342=ORIENTED_EDGE ( 'NONE', *, *, #7158, .T. ) ;
#3358=CARTESIAN_POINT ( 'NONE',  ( -2.387319993259524598, -4.036502139894371233, -0.8000000000000000444 ) ) ;
#3374=ADVANCED_FACE ( 'NONE', ( #12812 ), #9741, .F. ) ;
#3430=FACE_OUTER_BOUND ( 'NONE', #3744, .T. ) ;
#3433=DIRECTION ( 'NONE',  ( 0.000000000000000000, 0.000000000000000000, 1.000000000000000000 ) ) ;
#3448=DIRECTION ( 'NONE',  ( 0.000000000000000000, 0.000000000000000000, 1.000000000000000000 ) ) ;
#3456=VECTOR ( 'NONE', #3792, 1000.000000000000114 ) ;
#3461=VERTEX_POINT ( 'NONE', #4246 ) ;
#3467=CARTESIAN_POINT ( 'NONE',  ( -0.1038759689922479496, -3.348389132562988646, 0.000000000000000000 ) ) ;
#3477=AXIS2_PLACEMENT_3D ( 'NONE', #5325, #12069, #9186 ) ;
#3483=CARTESIAN_POINT ( 'NONE',  ( 0.000000000000000000, 0.4117131682837005258, -0.8000000000000000444 ) ) ;
#3614=UNCERTAINTY_MEASURE_WITH_UNIT (LENGTH_MEASURE( 1.000000000000000082E-05 ), #2042, 'distance_accuracy_value', 'NONE');
#3617=ORIENTED_EDGE ( 'NONE', *, *, #4217, .F. ) ;
#3625=DIRECTION ( 'NONE',  ( 1.000000000000000000, 0.000000000000000000, 0.000000000000000000 ) ) ;
#3626=CARTESIAN_POINT ( 'NONE',  ( -0.9999999999999997780, -4.273461295629625845, -0.8000000000000000444 ) ) ;
#3658=DIRECTION ( 'NONE',  ( 1.000000000000000000, 0.000000000000000000, 0.000000000000000000 ) ) ;
#3669=DIRECTION ( 'NONE',  ( 1.000000000000000000, 0.000000000000000000, 0.000000000000000000 ) ) ;
#3691=CARTESIAN_POINT ( 'NONE',  ( 0.000000000000000000, 0.4117131682837005258, 0.000000000000000000 ) ) ;
#3695=CARTESIAN_POINT ( 'NONE',  ( 0.1038759689922479496, -3.348389132562988646, 0.000000000000000000 ) ) ;
#3705=ORIENTED_EDGE ( 'NONE', *, *, #2166, .F. ) ;
#3735=CARTESIAN_POINT ( 'NONE',  ( -1.625004804578467077, -6.241943558307533557, -0.8000000000000000444 ) ) ;
#3741=EDGE_CURVE ( 'NONE', #7875, #10050, #5731, .T. ) ;
#3744=EDGE_LOOP ( 'NONE', ( #2875, #4769, #2119, #6842 ) ) ;
#3746=AXIS2_PLACEMENT_3D ( 'NONE', #1459, #1522, #5512 ) ;
#3760=CARTESIAN_POINT ( 'NONE',  ( 0.000000000000000000, 0.000000000000000000, -0.8000000000000000444 ) ) ;
#3787=DIRECTION ( 'NONE',  ( 0.000000000000000000, 0.000000000000000000, 1.000000000000000000 ) ) ;
#3792=DIRECTION ( 'NONE',  ( 0.03100775193798453039, -0.9995191440486532741, 0.000000000000000000 ) ) ;
#3826=VERTEX_POINT ( 'NONE', #6181 ) ;
#3846=EDGE_CURVE ( 'NONE', #10533, #1140, #4115, .T. ) ;
#3865=ORIENTED_EDGE ( 'NONE', *, *, #1307, .T. ) ;
#3874=DIRECTION ( 'NONE',  ( -0.000000000000000000, -0.000000000000000000, -1.000000000000000000 ) ) ;
#3875=ORIENTED_EDGE ( 'NONE', *, *, #1710, .T. ) ;
#3876=CIRCLE ( 'NONE', #8476, 0.5999999999999998668 ) ;
#3895=EDGE_CURVE ( 'NONE', #6695, #11510, #4481, .T. ) ;
#3899=EDGE_LOOP ( 'NONE', ( #11490, #5187, #478, #8574 ) ) ;
#3901=CARTESIAN_POINT ( 'NONE',  ( -2.179634403564815859, -5.614030811971695734, 0.000000000000000000 ) ) ;
#3936=DIRECTION ( 'NONE',  ( 1.000000000000000000, 0.000000000000000000, 0.000000000000000000 ) ) ;
#3958=LINE ( 'NONE', #1058, #6070 ) ;
#3969=VECTOR ( 'NONE', #3787, 1000.000000000000000 ) ;
#3976=ORIENTED_EDGE ( 'NONE', *, *, #12676, .F. ) ;
#3983=ORIENTED_EDGE ( 'NONE', *, *, #4725, .F. ) ;
#4021=ORIENTED_EDGE ( 'NONE', *, *, #9946, .T. ) ;
#4042=CARTESIAN_POINT ( 'NONE',  ( 1.436050757534458100, -5.516136167806656943, -0.8000000000000000444 ) ) ;
#4092=FACE_OUTER_BOUND ( 'NONE', #1678, .T. ) ;
#4094=CIRCLE ( 'NONE', #8680, 2.396199811936269963 ) ;
#4108=CARTESIAN_POINT ( 'NONE',  ( -0.1325741768533960641, -4.273461295629625845, -0.8000000000000000444 ) ) ;
#4115=CIRCLE ( 'NONE', #1389, 4.338286831716297698 ) ;
#4122=EDGE_CURVE ( 'NONE', #7384, #1569, #11528, .T. ) ;
#4160=LINE ( 'NONE', #11280, #9932 ) ;
#4173=CARTESIAN_POINT ( 'NONE',  ( 1.000000000000000000, -4.873461295629625489, -0.8000000000000000444 ) ) ;
#4217=EDGE_CURVE ( 'NONE', #11778, #4659, #912, .T. ) ;
#4246=CARTESIAN_POINT ( 'NONE',  ( 0.1698013801012111523, -5.473461295629626022, -0.8000000000000000444 ) ) ;
#4256=ORIENTED_EDGE ( 'NONE', *, *, #11576, .T. ) ;
#4272=ORIENTED_EDGE ( 'NONE', *, *, #7674, .T. ) ;
#4284=CARTESIAN_POINT ( 'NONE',  ( 1.625004804578465745, -6.241943558307532669, -0.8000000000000000444 ) ) ;
#4288=LINE ( 'NONE', #10164, #6146 ) ;
#4325=VERTEX_POINT ( 'NONE', #7734 ) ;
#4326=EDGE_CURVE ( 'NONE', #1479, #1569, #2771, .T. ) ;
#4332=LINE ( 'NONE', #11567, #4356 ) ;
#4356=VECTOR ( 'NONE', #5738, 1000.000000000000114 ) ;
#4373=ADVANCED_FACE ( 'NONE', ( #8123 ), #10073, .F. ) ;
#4380=ORIENTED_EDGE ( 'NONE', *, *, #6829, .F. ) ;
#4416=CARTESIAN_POINT ( 'NONE',  ( -0.9999999999999997780, -4.273461295629625845, -0.8000000000000000444 ) ) ;
#4424=ORIENTED_EDGE ( 'NONE', *, *, #7958, .T. ) ;
#4434=EDGE_LOOP ( 'NONE', ( #15, #12236, #7458, #4758 ) ) ;
#4437=ORIENTED_EDGE ( 'NONE', *, *, #4217, .T. ) ;
#4454=EDGE_LOOP ( 'NONE', ( #2690, #6946, #6484, #10355 ) ) ;
#4481=LINE ( 'NONE', #7359, #2655 ) ;
#4504=ORIENTED_EDGE ( 'NONE', *, *, #10546, .F. ) ;
#4516=ORIENTED_EDGE ( 'NONE', *, *, #3056, .T. ) ;
#4563=DIRECTION ( 'NONE',  ( 0.000000000000000000, 0.000000000000000000, 1.000000000000000000 ) ) ;
#4570=ORIENTED_EDGE ( 'NONE', *, *, #10835, .F. ) ;
#4576=ORIENTED_EDGE ( 'NONE', *, *, #11395, .T. ) ;
#4609=CARTESIAN_POINT ( 'NONE',  ( 1.000000000000000000, -4.873461295629625489, -0.8000000000000000444 ) ) ;
#4615=CARTESIAN_POINT ( 'NONE',  ( -3.350000000000000089, 4.102566777143633281E-16, -0.8000000000000000444 ) ) ;
#4634=VERTEX_POINT ( 'NONE', #1010 ) ;
#4635=EDGE_CURVE ( 'NONE', #3826, #12707, #2071, .T. ) ;
#4643=CARTESIAN_POINT ( 'NONE',  ( -0.2000000000000000111, -6.446898479113814417, 0.000000000000000000 ) ) ;
#4659=VERTEX_POINT ( 'NONE', #11820 ) ;
#4692=DIRECTION ( 'NONE',  ( -1.000000000000000000, 0.000000000000000000, 0.000000000000000000 ) ) ;
#4701=CARTESIAN_POINT ( 'NONE',  ( 2.387319993259524598, -4.036502139894371233, -0.8000000000000000444 ) ) ;
#4704=DIRECTION ( 'NONE',  ( 0.000000000000000000, 0.000000000000000000, 1.000000000000000000 ) ) ;
#4725=EDGE_CURVE ( 'NONE', #7369, #4634, #6112, .T. ) ;
#4729=DIRECTION ( 'NONE',  ( 0.000000000000000000, 0.000000000000000000, 1.000000000000000000 ) ) ;
#4749=VECTOR ( 'NONE', #7102, 1000.000000000000114 ) ;
#4758=ORIENTED_EDGE ( 'NONE', *, *, #6379, .F. ) ;
#4769=ORIENTED_EDGE ( 'NONE', *, *, #6371, .F. ) ;
#4795=AXIS2_PLACEMENT_3D ( 'NONE', #12247, #11120, #3294 ) ;
#4818=DIRECTION ( 'NONE',  ( 0.000000000000000000, 0.000000000000000000, 1.000000000000000000 ) ) ;
#4824=DIRECTION ( 'NONE',  ( 0.000000000000000000, 0.000000000000000000, 1.000000000000000000 ) ) ;
#4849=ORIENTED_EDGE ( 'NONE', *, *, #10959, .F. ) ;
#4866=DIRECTION ( 'NONE',  ( -0.9995191440486532741, -0.03100775193798452692, 0.000000000000000000 ) ) ;
#4886=DIRECTION ( 'NONE',  ( 1.000000000000000000, 0.000000000000000000, 0.000000000000000000 ) ) ;
#4926=DIRECTION ( 'NONE',  ( 1.000000000000000000, 0.000000000000000000, 0.000000000000000000 ) ) ;
#4938=DIRECTION ( 'NONE',  ( 0.000000000000000000, 0.000000000000000000, 1.000000000000000000 ) ) ;
#4943=EDGE_CURVE ( 'NONE', #169, #1744, #8098, .T. ) ;
#4944=CARTESIAN_POINT ( 'NONE',  ( -2.179634403564815859, -5.614030811971695734, -0.8000000000000000444 ) ) ;
#4961=DIRECTION ( 'NONE',  ( -0.000000000000000000, 1.000000000000000000, 0.000000000000000000 ) ) ;
#4981=EDGE_CURVE ( 'NONE', #1892, #1472, #8725, .T. ) ;
#5002=EDGE_CURVE ( 'NONE', #3280, #5034, #7881, .T. ) ;
#5009=DIRECTION ( 'NONE',  ( 0.1305261922200528224, 0.9914448613738103822, -0.000000000000000000 ) ) ;
#5015=AXIS2_PLACEMENT_3D ( 'NONE', #11684, #4818, #8804 ) ;
#5034=VERTEX_POINT ( 'NONE', #3901 ) ;
#5072=AXIS2_PLACEMENT_3D ( 'NONE', #1258, #6292, #10155 ) ;
#5084=ORIENTED_EDGE ( 'NONE', *, *, #2430, .F. ) ;
#5094=SHAPE_DEFINITION_REPRESENTATION ( #9501, #9014 ) ;
#5098=ORIENTED_EDGE ( 'NONE', *, *, #6379, .T. ) ;
#5106=EDGE_CURVE ( 'NONE', #85, #1209, #7475, .T. ) ;
#5113=ORIENTED_EDGE ( 'NONE', *, *, #1198, .F. ) ;
#5124=DIRECTION ( 'NONE',  ( 1.000000000000000000, 0.000000000000000000, 0.000000000000000000 ) ) ;
#5139=DIRECTION ( 'NONE',  ( 0.000000000000000000, 0.000000000000000000, 1.000000000000000000 ) ) ;
#5165=CYLINDRICAL_SURFACE ( 'NONE', #6747, 3.350000000000000089 ) ;
#5182=CARTESIAN_POINT ( 'NONE',  ( 0.1698013801012111523, -5.473461295629626022, 0.000000000000000000 ) ) ;
#5187=ORIENTED_EDGE ( 'NONE', *, *, #9714, .T. ) ;
#5191=PLANE ( 'NONE',  #2702 ) ;
#5232=CARTESIAN_POINT ( 'NONE',  ( 0.000000000000000000, 0.000000000000000000, -0.8000000000000000444 ) ) ;
#5245=AXIS2_PLACEMENT_3D ( 'NONE', #8593, #11720, #1781 ) ;
#5248=DIRECTION ( 'NONE',  ( 1.000000000000000000, 0.000000000000000000, 0.000000000000000000 ) ) ;
#5258=LINE ( 'NONE', #4284, #11885 ) ;
#5270=DIRECTION ( 'NONE',  ( 0.000000000000000000, 0.000000000000000000, 1.000000000000000000 ) ) ;
#5272=ADVANCED_FACE ( 'NONE', ( #3430 ), #2645, .T. ) ;
#5288=ORIENTED_EDGE ( 'NONE', *, *, #12761, .T. ) ;
#5321=AXIS2_PLACEMENT_3D ( 'NONE', #3760, #8913, #11729 ) ;
#5325=CARTESIAN_POINT ( 'NONE',  ( -0.1038759689922479496, -3.348389132562988646, -0.8000000000000000444 ) ) ;
#5345=ORIENTED_EDGE ( 'NONE', *, *, #11274, .F. ) ;
#5346=ADVANCED_FACE ( 'NONE', ( #1657 ), #11400, .T. ) ;
#5378=DIRECTION ( 'NONE',  ( 1.000000000000000000, 0.000000000000000000, 0.000000000000000000 ) ) ;
#5401=PLANE ( 'NONE',  #7101 ) ;
#5407=ADVANCED_FACE ( 'NONE', ( #7073 ), #6149, .F. ) ;
#5412=PRODUCT_DEFINITION_CONTEXT ( 'detailed design', #3183, 'design' ) ;
#5421=EDGE_LOOP ( 'NONE', ( #6119, #8184, #7466, #7187 ) ) ;
#5424=ORIENTED_EDGE ( 'NONE', *, *, #3846, .F. ) ;
#5425=CARTESIAN_POINT ( 'NONE',  ( 1.000000000000000000, -4.873461295629625489, 0.000000000000000000 ) ) ;
#5428=VECTOR ( 'NONE', #4563, 1000.000000000000000 ) ;
#5432=DIRECTION ( 'NONE',  ( 0.03100775193798453039, 0.9995191440486532741, -0.000000000000000000 ) ) ;
#5441=DIRECTION ( 'NONE',  ( 1.000000000000000000, 0.000000000000000000, 0.000000000000000000 ) ) ;
#5444=DIRECTION ( 'NONE',  ( 0.000000000000000000, 0.000000000000000000, 1.000000000000000000 ) ) ;
#5454=EDGE_CURVE ( 'NONE', #5809, #11221, #7593, .T. ) ;
#5455=VERTEX_POINT ( 'NONE', #10344 ) ;
#5463=VERTEX_POINT ( 'NONE', #1507 ) ;
#5477=VERTEX_POINT ( 'NONE', #11316 ) ;
#5499=CARTESIAN_POINT ( 'NONE',  ( 0.1038759689922479496, -3.348389132562988646, 0.000000000000000000 ) ) ;
#5512=DIRECTION ( 'NONE',  ( 0.1305261922200528224, 0.9914448613738103822, 0.000000000000000000 ) ) ;
#5523=DIRECTION ( 'NONE',  ( 0.9995191440486532741, -0.03100775193798452692, 0.000000000000000000 ) ) ;
#5529=DIRECTION ( 'NONE',  ( 0.000000000000000000, 0.000000000000000000, 1.000000000000000000 ) ) ;
#5585=DIRECTION ( 'NONE',  ( 0.000000000000000000, 0.000000000000000000, 1.000000000000000000 ) ) ;
#5631=VECTOR ( 'NONE', #10799, 1000.000000000000000 ) ;
#5650=PLANE ( 'NONE',  #1548 ) ;
#5691=CARTESIAN_POINT ( 'NONE',  ( 0.000000000000000000, 0.4117131682837005258, -0.8000000000000000444 ) ) ;
#5704=AXIS2_PLACEMENT_3D ( 'NONE', #8997, #4824, #4886 ) ;
#5705=LINE ( 'NONE', #1652, #8390 ) ;
#5714=CYLINDRICAL_SURFACE ( 'NONE', #5321, 3.350000000000000089 ) ;
#5724=EDGE_CURVE ( 'NONE', #12575, #1209, #2947, .T. ) ;
#5728=DIRECTION ( 'NONE',  ( 0.000000000000000000, 0.000000000000000000, 1.000000000000000000 ) ) ;
#5731=LINE ( 'NONE', #2984, #8508 ) ;
#5738=DIRECTION ( 'NONE',  ( 0.03100775193798453039, 0.9995191440486532741, -0.000000000000000000 ) ) ;
#5748=PLANE ( 'NONE',  #6805 ) ;
#5808=CARTESIAN_POINT ( 'NONE',  ( -0.1698013801012111523, -5.473461295629626022, 0.000000000000000000 ) ) ;
#5809=VERTEX_POINT ( 'NONE', #11039 ) ;
#5812=ORIENTED_EDGE ( 'NONE', *, *, #11735, .T. ) ;
#5813=DIRECTION ( 'NONE',  ( 1.000000000000000000, 0.000000000000000000, 0.000000000000000000 ) ) ;
#5825=DIRECTION ( 'NONE',  ( 1.000000000000000000, 0.000000000000000000, 0.000000000000000000 ) ) ;
#5829=EDGE_LOOP ( 'NONE', ( #3976, #5345, #9432, #10892, #3865, #10472, #3875, #9237, #12490, #4576, #359, #4272, #9837, #12826, #10798, #3122, #6332, #227, #10800, #8411, #3342, #1619, #2338, #1716, #2439 ) ) ;
#5836=DIRECTION ( 'NONE',  ( 0.03100775193798453039, -0.9995191440486532741, 0.000000000000000000 ) ) ;
#5929=DIRECTION ( 'NONE',  ( 1.000000000000000000, 0.000000000000000000, 0.000000000000000000 ) ) ;
#5945=ORIENTED_EDGE ( 'NONE', *, *, #8210, .T. ) ;
#5964=ORIENTED_EDGE ( 'NONE', *, *, #5454, .F. ) ;
#5998=SHAPE_REPRESENTATION_RELATIONSHIP ( 'NONE' , 'NONE' ,  #9014, #12938 ) ;
#6022=VECTOR ( 'NONE', #12263, 1000.000000000000000 ) ;
#6049=AXIS2_PLACEMENT_3D ( 'NONE', #12809, #7839, #5929 ) ;
#6058=ORIENTED_EDGE ( 'NONE', *, *, #6326, .F. ) ;
#6070=VECTOR ( 'NONE', #12058, 1000.000000000000000 ) ;
#6081=DIRECTION ( 'NONE',  ( 0.000000000000000000, 0.000000000000000000, 1.000000000000000000 ) ) ;
#6105=DIRECTION ( 'NONE',  ( 0.000000000000000000, 0.000000000000000000, -1.000000000000000000 ) ) ;
#6112=LINE ( 'NONE', #9193, #4749 ) ;
#6119=ORIENTED_EDGE ( 'NONE', *, *, #7874, .T. ) ;
#6146=VECTOR ( 'NONE', #6301, 1000.000000000000000 ) ;
#6149=CYLINDRICAL_SURFACE ( 'NONE', #8537, 2.396199811936270407 ) ;
#6150=EDGE_CURVE ( 'NONE', #1892, #5455, #12802, .T. ) ;
#6162=FACE_OUTER_BOUND ( 'NONE', #8558, .T. ) ;
#6178=CARTESIAN_POINT ( 'NONE',  ( -4.338286831716297698, 0.4117131682837010809, -0.8000000000000000444 ) ) ;
#6181=CARTESIAN_POINT ( 'NONE',  ( 2.179634403564814971, -5.614030811971695734, 0.000000000000000000 ) ) ;
#6183=ORIENTED_EDGE ( 'NONE', *, *, #9652, .T. ) ;
#6201=VERTEX_POINT ( 'NONE', #11690 ) ;
#6247=VERTEX_POINT ( 'NONE', #10292 ) ;
#6256=ORIENTED_EDGE ( 'NONE', *, *, #9643, .T. ) ;
#6292=DIRECTION ( 'NONE',  ( 0.000000000000000000, 0.000000000000000000, 1.000000000000000000 ) ) ;
#6299=ADVANCED_FACE ( 'NONE', ( #2385 ), #5191, .F. ) ;
#6301=DIRECTION ( 'NONE',  ( 0.000000000000000000, 0.000000000000000000, 1.000000000000000000 ) ) ;
#6303=DIRECTION ( 'NONE',  ( 0.000000000000000000, 0.000000000000000000, 1.000000000000000000 ) ) ;
#6314=ADVANCED_FACE ( 'NONE', ( #4092 ), #12065, .T. ) ;
#6324=ORIENTED_EDGE ( 'NONE', *, *, #7958, .F. ) ;
#6326=EDGE_CURVE ( 'NONE', #1744, #12575, #9591, .T. ) ;
#6332=ORIENTED_EDGE ( 'NONE', *, *, #6543, .T. ) ;
#6357=EDGE_CURVE ( 'NONE', #10050, #8873, #204, .T. ) ;
#6364=CARTESIAN_POINT ( 'NONE',  ( 1.000000000000000000, -5.473461295629626022, -0.8000000000000000444 ) ) ;
#6367=CARTESIAN_POINT ( 'NONE',  ( 0.1325741768533960085, -4.273461295629625845, -0.8000000000000000444 ) ) ;
#6371=EDGE_CURVE ( 'NONE', #1472, #9206, #5258, .T. ) ;
#6373=AXIS2_PLACEMENT_3D ( 'NONE', #12477, #5728, #4692 ) ;
#6379=EDGE_CURVE ( 'NONE', #6201, #12851, #398, .T. ) ;
#6396=ADVANCED_FACE ( 'NONE', ( #7544 ), #11402, .T. ) ;
#6409=CARTESIAN_POINT ( 'NONE',  ( -1.000000000000000000, -4.873461295629625489, 0.000000000000000000 ) ) ;
#6429=DIRECTION ( 'NONE',  ( 1.000000000000000000, 0.000000000000000000, 0.000000000000000000 ) ) ;
#6432=DIRECTION ( 'NONE',  ( -0.000000000000000000, 1.000000000000000000, 0.000000000000000000 ) ) ;
#6442=ADVANCED_FACE ( 'NONE', ( #2516 ), #12521, .T. ) ;
#6475=EDGE_LOOP ( 'NONE', ( #12155, #4516, #110, #3983, #11644, #12937, #8216, #6324, #9498, #881, #5945, #1921, #6058, #7474, #3705, #9275, #11575, #5424, #12476, #1237, #7654, #9259, #433, #1086, #6256 ) ) ;
#6484=ORIENTED_EDGE ( 'NONE', *, *, #6326, .T. ) ;
#6499=AXIS2_PLACEMENT_3D ( 'NONE', #5425, #2306, #8385 ) ;
#6502=ORIENTED_EDGE ( 'NONE', *, *, #7427, .T. ) ;
#6542=EDGE_LOOP ( 'NONE', ( #4849, #710, #8452, #1097 ) ) ;
#6543=EDGE_CURVE ( 'NONE', #1209, #8873, #2165, .T. ) ;
#6548=VERTEX_POINT ( 'NONE', #12171 ) ;
#6625=CARTESIAN_POINT ( 'NONE',  ( 0.000000000000000000, 0.4117131682837005258, 0.000000000000000000 ) ) ;
#6695=VERTEX_POINT ( 'NONE', #8599 ) ;
#6713=ORIENTED_EDGE ( 'NONE', *, *, #7105, .T. ) ;
#6727=( GEOMETRIC_REPRESENTATION_CONTEXT ( 3 ) GLOBAL_UNCERTAINTY_ASSIGNED_CONTEXT ( ( #3614 ) ) GLOBAL_UNIT_ASSIGNED_CONTEXT ( ( #2042, #7991, #2173 ) ) REPRESENTATION_CONTEXT ( 'NONE', 'WORKASPACE' ) );
#6744=CARTESIAN_POINT ( 'NONE',  ( -0.9999999999999997780, -4.273461295629625845, 0.000000000000000000 ) ) ;
#6747=AXIS2_PLACEMENT_3D ( 'NONE', #5232, #6081, #8248 ) ;
#6788=CARTESIAN_POINT ( 'NONE',  ( 0.1038759689922479496, -3.348389132562988646, 0.000000000000000000 ) ) ;
#6791=CARTESIAN_POINT ( 'NONE',  ( -0.9999999999999997780, -4.273461295629625845, -0.8000000000000000444 ) ) ;
#6795=VERTEX_POINT ( 'NONE', #11467 ) ;
#6801=LINE ( 'NONE', #11650, #86 ) ;
#6805=AXIS2_PLACEMENT_3D ( 'NONE', #6791, #4961, #2020 ) ;
#6822=DIRECTION ( 'NONE',  ( 0.000000000000000000, 0.000000000000000000, 1.000000000000000000 ) ) ;
#6829=EDGE_CURVE ( 'NONE', #9537, #8099, #2963, .T. ) ;
#6833=APPLICATION_CONTEXT ( 'automotive_design' ) ;
#6838=DIRECTION ( 'NONE',  ( -0.000000000000000000, -0.000000000000000000, 1.000000000000000000 ) ) ;
#6842=ORIENTED_EDGE ( 'NONE', *, *, #2054, .T. ) ;
#6897=DIRECTION ( 'NONE',  ( -0.000000000000000000, -0.000000000000000000, 1.000000000000000000 ) ) ;
#6912=CARTESIAN_POINT ( 'NONE',  ( -2.179634403564815859, -5.614030811971695734, -0.8000000000000000444 ) ) ;
#6915=EDGE_LOOP ( 'NONE', ( #11497, #546, #9411, #3617 ) ) ;
#6928=ORIENTED_EDGE ( 'NONE', *, *, #2166, .T. ) ;
#6946=ORIENTED_EDGE ( 'NONE', *, *, #11735, .F. ) ;
#6954=DIRECTION ( 'NONE',  ( 0.000000000000000000, 0.000000000000000000, 1.000000000000000000 ) ) ;
#6991=CIRCLE ( 'NONE', #7822, 3.350000000000000089 ) ;
#7034=EDGE_CURVE ( 'NONE', #11221, #3280, #10226, .T. ) ;
#7044=DIRECTION ( 'NONE',  ( -1.000000000000000000, 0.000000000000000000, 0.000000000000000000 ) ) ;
#7057=ORIENTED_EDGE ( 'NONE', *, *, #8210, .F. ) ;
#7073=FACE_OUTER_BOUND ( 'NONE', #9663, .T. ) ;
#7087=UNCERTAINTY_MEASURE_WITH_UNIT (LENGTH_MEASURE( 1.000000000000000082E-05 ), #1952, 'distance_accuracy_value', 'NONE');
#7094=VECTOR ( 'NONE', #973, 1000.000000000000000 ) ;
#7101=AXIS2_PLACEMENT_3D ( 'NONE', #11294, #1545, #12407 ) ;
#7102=DIRECTION ( 'NONE',  ( 0.03100775193798453039, -0.9995191440486532741, 0.000000000000000000 ) ) ;
#7105=EDGE_CURVE ( 'NONE', #9809, #3280, #9732, .T. ) ;
#7113=CARTESIAN_POINT ( 'NONE',  ( -1.000000000000000000, -5.473461295629626022, 0.000000000000000000 ) ) ;
#7121=CIRCLE ( 'NONE', #5245, 0.5999999999999998668 ) ;
#7148=CIRCLE ( 'NONE', #1508, 0.5999999999999999778 ) ;
#7158=EDGE_CURVE ( 'NONE', #1479, #12851, #4332, .T. ) ;
#7187=ORIENTED_EDGE ( 'NONE', *, *, #12676, .T. ) ;
#7225=DIRECTION ( 'NONE',  ( 0.000000000000000000, 0.000000000000000000, -1.000000000000000000 ) ) ;
#7230=AXIS2_PLACEMENT_3D ( 'NONE', #72, #8004, #7804 ) ;
#7255=EDGE_LOOP ( 'NONE', ( #9563, #8777, #10726, #2700 ) ) ;
#7262=EDGE_LOOP ( 'NONE', ( #11931, #7057, #8489, #7320 ) ) ;
#7269=PLANE ( 'NONE',  #12790 ) ;
#7320=ORIENTED_EDGE ( 'NONE', *, *, #6357, .T. ) ;
#7343=CYLINDRICAL_SURFACE ( 'NONE', #5072, 0.5999999999999998668 ) ;
#7359=CARTESIAN_POINT ( 'NONE',  ( 1.000000000000000000, -5.473461295629626022, -0.8000000000000000444 ) ) ;
#7365=AXIS2_PLACEMENT_3D ( 'NONE', #8825, #8952, #1958 ) ;
#7366=LINE ( 'NONE', #2402, #8968 ) ;
#7369=VERTEX_POINT ( 'NONE', #11886 ) ;
#7384=VERTEX_POINT ( 'NONE', #10778 ) ;
#7386=CARTESIAN_POINT ( 'NONE',  ( -4.338286831716297698, 0.4117131682837010809, -0.8000000000000000444 ) ) ;
#7401=PRODUCT_DEFINITION_FORMATION_WITH_SPECIFIED_SOURCE ( 'ANY', '', #12209, .NOT_KNOWN. ) ;
#7427=EDGE_CURVE ( 'NONE', #6795, #12707, #7366, .T. ) ;
#7458=ORIENTED_EDGE ( 'NONE', *, *, #12524, .F. ) ;
#7466=ORIENTED_EDGE ( 'NONE', *, *, #7830, .T. ) ;
#7473=ADVANCED_FACE ( 'NONE', ( #1410 ), #10376, .F. ) ;
#7474=ORIENTED_EDGE ( 'NONE', *, *, #4943, .F. ) ;
#7475=CIRCLE ( 'NONE', #10186, 6.450000000000001066 ) ;
#7487=LINE ( 'NONE', #8604, #10775 ) ;
#7492=VECTOR ( 'NONE', #8767, 1000.000000000000000 ) ;
#7518=AXIS2_PLACEMENT_3D ( 'NONE', #2252, #11260, #5248 ) ;
#7544=FACE_OUTER_BOUND ( 'NONE', #9614, .T. ) ;
#7548=LINE ( 'NONE', #11534, #3247 ) ;
#7588=DIRECTION ( 'NONE',  ( 1.000000000000000000, 0.000000000000000000, 0.000000000000000000 ) ) ;
#7593=LINE ( 'NONE', #515, #11447 ) ;
#7623=EDGE_LOOP ( 'NONE', ( #10669, #4504, #9752, #5812 ) ) ;
#7639=DIRECTION ( 'NONE',  ( 0.1305261922200528224, 0.9914448613738103822, -0.000000000000000000 ) ) ;
#7654=ORIENTED_EDGE ( 'NONE', *, *, #12761, .F. ) ;
#7668=VERTEX_POINT ( 'NONE', #10503 ) ;
#7674=EDGE_CURVE ( 'NONE', #5477, #11221, #8241, .T. ) ;
#7680=VECTOR ( 'NONE', #1734, 999.9999999999998863 ) ;
#7691=CARTESIAN_POINT ( 'NONE',  ( 0.000000000000000000, 0.4117131682837005258, 0.000000000000000000 ) ) ;
#7714=ORIENTED_EDGE ( 'NONE', *, *, #7034, .F. ) ;
#7718=CARTESIAN_POINT ( 'NONE',  ( 3.068288344391240763, -2.655262421758693314, -0.8000000000000000444 ) ) ;
#7734=CARTESIAN_POINT ( 'NONE',  ( 3.350000000000000089, 0.000000000000000000, 0.000000000000000000 ) ) ;
#7771=FACE_OUTER_BOUND ( 'NONE', #7255, .T. ) ;
#7772=CARTESIAN_POINT ( 'NONE',  ( -3.350000000000000089, 4.102566777143633281E-16, 0.000000000000000000 ) ) ;
#7804=DIRECTION ( 'NONE',  ( 1.000000000000000000, 0.000000000000000000, 0.000000000000000000 ) ) ;
#7807=LINE ( 'NONE', #4615, #2954 ) ;
#7814=AXIS2_PLACEMENT_3D ( 'NONE', #6625, #5585, #11471 ) ;
#7822=AXIS2_PLACEMENT_3D ( 'NONE', #11798, #990, #4926 ) ;
#7830=EDGE_CURVE ( 'NONE', #6548, #1939, #11741, .T. ) ;
#7839=DIRECTION ( 'NONE',  ( 0.000000000000000000, 0.000000000000000000, 1.000000000000000000 ) ) ;
#7859=ORIENTED_EDGE ( 'NONE', *, *, #8275, .T. ) ;
#7874=EDGE_CURVE ( 'NONE', #8099, #4634, #11140, .T. ) ;
#7875=VERTEX_POINT ( 'NONE', #140 ) ;
#7881=LINE ( 'NONE', #11933, #7680 ) ;
#7886=EDGE_CURVE ( 'NONE', #362, #1479, #4288, .T. ) ;
#7889=LINE ( 'NONE', #2983, #9200 ) ;
#7901=AXIS2_PLACEMENT_3D ( 'NONE', #397, #12587, #12324 ) ;
#7906=CARTESIAN_POINT ( 'NONE',  ( -2.387319993259524598, -4.036502139894371233, -0.8000000000000000444 ) ) ;
#7917=PLANE ( 'NONE',  #9305 ) ;
#7920=VECTOR ( 'NONE', #12384, 1000.000000000000000 ) ;
#7933=ORIENTED_EDGE ( 'NONE', *, *, #988, .F. ) ;
#7943=CARTESIAN_POINT ( 'NONE',  ( 0.1038759689922479496, -3.348389132562988646, -0.8000000000000000444 ) ) ;
#7958=EDGE_CURVE ( 'NONE', #362, #6201, #7548, .T. ) ;
#7974=AXIS2_PLACEMENT_3D ( 'NONE', #5691, #12434, #7588 ) ;
#7984=LINE ( 'NONE', #11968, #7094 ) ;
#7991=( NAMED_UNIT ( * ) PLANE_ANGLE_UNIT ( ) SI_UNIT ( $, .RADIAN. ) );
#7998=ADVANCED_FACE ( 'NONE', ( #11405 ), #1596, .F. ) ;
#8004=DIRECTION ( 'NONE',  ( 0.000000000000000000, 0.000000000000000000, 1.000000000000000000 ) ) ;
#8006=FACE_OUTER_BOUND ( 'NONE', #1713, .T. ) ;
#8019=MECHANICAL_DESIGN_GEOMETRIC_PRESENTATION_REPRESENTATION('',(#10095),#9472);
#8031=DIRECTION ( 'NONE',  ( 0.000000000000000000, 0.000000000000000000, 1.000000000000000000 ) ) ;
#8098=CIRCLE ( 'NONE', #10813, 0.7499999999999997780 ) ;
#8099=VERTEX_POINT ( 'NONE', #8909 ) ;
#8106=CARTESIAN_POINT ( 'NONE',  ( -0.9999999999999997780, -4.273461295629625845, 0.000000000000000000 ) ) ;
#8123=FACE_OUTER_BOUND ( 'NONE', #10281, .T. ) ;
#8133=CYLINDRICAL_SURFACE ( 'NONE', #1776, 0.7499999999999997780 ) ;
#8184=ORIENTED_EDGE ( 'NONE', *, *, #11359, .F. ) ;
#8210=EDGE_CURVE ( 'NONE', #7875, #5463, #8846, .T. ) ;
#8216=ORIENTED_EDGE ( 'NONE', *, *, #11202, .F. ) ;
#8241=CIRCLE ( 'NONE', #1341, 4.338286831716297698 ) ;
#8248=DIRECTION ( 'NONE',  ( 1.000000000000000000, 0.000000000000000000, 0.000000000000000000 ) ) ;
#8273=DIRECTION ( 'NONE',  ( 0.000000000000000000, 0.000000000000000000, 1.000000000000000000 ) ) ;
#8275=EDGE_CURVE ( 'NONE', #12575, #5463, #1447, .T. ) ;
#8313=EDGE_CURVE ( 'NONE', #362, #7384, #6801, .T. ) ;
#8345=VECTOR ( 'NONE', #5836, 1000.000000000000114 ) ;
#8353=CIRCLE ( 'NONE', #7518, 2.396199811936270407 ) ;
#8366=EDGE_CURVE ( 'NONE', #12707, #4659, #4094, .T. ) ;
#8369=CARTESIAN_POINT ( 'NONE',  ( 2.387319993259524598, -4.036502139894371233, 0.000000000000000000 ) ) ;
#8377=DIRECTION ( 'NONE',  ( 1.000000000000000000, 0.000000000000000000, 0.000000000000000000 ) ) ;
#8385=DIRECTION ( 'NONE',  ( 1.000000000000000000, 0.000000000000000000, 0.000000000000000000 ) ) ;
#8390=VECTOR ( 'NONE', #1586, 1000.000000000000000 ) ;
#8396=ADVANCED_FACE ( 'NONE', ( #10668 ), #7917, .T. ) ;
#8411=ORIENTED_EDGE ( 'NONE', *, *, #4326, .F. ) ;
#8412=FACE_OUTER_BOUND ( 'NONE', #9474, .T. ) ;
#8413=CARTESIAN_POINT ( 'NONE',  ( -1.436050757534458100, -5.516136167806656943, -0.8000000000000000444 ) ) ;
#8436=VERTEX_POINT ( 'NONE', #9149 ) ;
#8437=AXIS2_PLACEMENT_3D ( 'NONE', #12560, #4704, #12684 ) ;
#8452=ORIENTED_EDGE ( 'NONE', *, *, #6150, .T. ) ;
#8476=AXIS2_PLACEMENT_3D ( 'NONE', #1084, #10902, #8817 ) ;
#8489=ORIENTED_EDGE ( 'NONE', *, *, #3741, .T. ) ;
#8508=VECTOR ( 'NONE', #6838, 1000.000000000000000 ) ;
#8517=VECTOR ( 'NONE', #10737, 1000.000000000000000 ) ;
#8537=AXIS2_PLACEMENT_3D ( 'NONE', #11055, #12177, #1110 ) ;
#8553=AXIS2_PLACEMENT_3D ( 'NONE', #1129, #11074, #3112 ) ;
#8558=EDGE_LOOP ( 'NONE', ( #10479, #1039, #10251, #4256 ) ) ;
#8574=ORIENTED_EDGE ( 'NONE', *, *, #7830, .F. ) ;
#8593=CARTESIAN_POINT ( 'NONE',  ( 1.000000000000000000, -4.873461295629625489, 0.000000000000000000 ) ) ;
#8599=CARTESIAN_POINT ( 'NONE',  ( 1.000000000000000000, -5.473461295629626022, -0.8000000000000000444 ) ) ;
#8603=DIRECTION ( 'NONE',  ( 0.000000000000000000, -0.000000000000000000, 1.000000000000000000 ) ) ;
#8604=CARTESIAN_POINT ( 'NONE',  ( -2.387319993259524598, -4.036502139894371233, -0.8000000000000000444 ) ) ;
#8647=DIRECTION ( 'NONE',  ( -1.000000000000000000, -0.000000000000000000, -0.000000000000000000 ) ) ;
#8671=AXIS2_PLACEMENT_3D ( 'NONE', #12119, #12053, #8377 ) ;
#8680=AXIS2_PLACEMENT_3D ( 'NONE', #780, #8895, #3936 ) ;
#8695=EDGE_LOOP ( 'NONE', ( #4570, #213, #1303, #5113 ) ) ;
#8724=FACE_OUTER_BOUND ( 'NONE', #8695, .T. ) ;
#8725=CIRCLE ( 'NONE', #9769, 6.450000000000001066 ) ;
#8767=DIRECTION ( 'NONE',  ( 0.000000000000000000, 0.000000000000000000, 1.000000000000000000 ) ) ;
#8777=ORIENTED_EDGE ( 'NONE', *, *, #2114, .T. ) ;
#8804=DIRECTION ( 'NONE',  ( 1.000000000000000000, 0.000000000000000000, 0.000000000000000000 ) ) ;
#8817=DIRECTION ( 'NONE',  ( 1.000000000000000000, 0.000000000000000000, 0.000000000000000000 ) ) ;
#8825=CARTESIAN_POINT ( 'NONE',  ( 0.000000000000000000, 0.000000000000000000, 0.000000000000000000 ) ) ;
#8835=ORIENTED_EDGE ( 'NONE', *, *, #1100, .T. ) ;
#8846=LINE ( 'NONE', #1854, #1987 ) ;
#8853=DIRECTION ( 'NONE',  ( 0.03100775193798452692, -0.9995191440486532741, 0.000000000000000000 ) ) ;
#8868=CIRCLE ( 'NONE', #290, 3.350000000000000089 ) ;
#8873=VERTEX_POINT ( 'NONE', #5808 ) ;
#8877=CIRCLE ( 'NONE', #6373, 0.7499999999999997780 ) ;
#8886=DIRECTION ( 'NONE',  ( 0.000000000000000000, 0.000000000000000000, 1.000000000000000000 ) ) ;
#8895=DIRECTION ( 'NONE',  ( -0.000000000000000000, -0.000000000000000000, -1.000000000000000000 ) ) ;
#8909=CARTESIAN_POINT ( 'NONE',  ( 0.1325741768533959530, -4.273461295629625845, 0.000000000000000000 ) ) ;
#8913=DIRECTION ( 'NONE',  ( 0.000000000000000000, 0.000000000000000000, 1.000000000000000000 ) ) ;
#8952=DIRECTION ( 'NONE',  ( -0.000000000000000000, -0.000000000000000000, -1.000000000000000000 ) ) ;
#8968=VECTOR ( 'NONE', #5139, 1000.000000000000000 ) ;
#8985=VECTOR ( 'NONE', #9384, 1000.000000000000114 ) ;
#8991=CARTESIAN_POINT ( 'NONE',  ( 4.338286831716297698, 0.4117131682837005258, -0.8000000000000000444 ) ) ;
#8997=CARTESIAN_POINT ( 'NONE',  ( 0.000000000000000000, 0.000000000000000000, 0.000000000000000000 ) ) ;
#9014=SHAPE_REPRESENTATION ( 'circlip for shafts normal_din_Circlip DIN 471 - 7 x 0.8', ( #5704 ), #1107 ) ;
#9027=ORIENTED_EDGE ( 'NONE', *, *, #9374, .T. ) ;
#9043=CARTESIAN_POINT ( 'NONE',  ( 0.1698013801012111523, -5.473461295629626022, -0.8000000000000000444 ) ) ;
#9078=CARTESIAN_POINT ( 'NONE',  ( 0.000000000000000000, 0.000000000000000000, 0.000000000000000000 ) ) ;
#9085=ORIENTED_EDGE ( 'NONE', *, *, #7874, .F. ) ;
#9096=CARTESIAN_POINT ( 'NONE',  ( -1.000000000000000000, -4.873461295629625489, -0.8000000000000000444 ) ) ;
#9105=FACE_OUTER_BOUND ( 'NONE', #7623, .T. ) ;
#9134=DIRECTION ( 'NONE',  ( 0.000000000000000000, 0.000000000000000000, 1.000000000000000000 ) ) ;
#9138=( LENGTH_UNIT ( ) NAMED_UNIT ( * ) SI_UNIT ( .MILLI., .METRE. ) );
#9149=CARTESIAN_POINT ( 'NONE',  ( 3.350000000000000089, 0.000000000000000000, -0.8000000000000000444 ) ) ;
#9155=CARTESIAN_POINT ( 'NONE',  ( -0.1038759689922479496, -3.348389132562988646, 0.000000000000000000 ) ) ;
#9186=DIRECTION ( 'NONE',  ( 0.03100775193798452692, 0.9995191440486532741, 0.000000000000000000 ) ) ;
#9193=CARTESIAN_POINT ( 'NONE',  ( 0.1038759689922479496, -3.348389132562988646, -0.8000000000000000444 ) ) ;
#9200=VECTOR ( 'NONE', #11016, 1000.000000000000000 ) ;
#9206=VERTEX_POINT ( 'NONE', #2596 ) ;
#9207=EDGE_LOOP ( 'NONE', ( #12022, #12630, #11625, #323 ) ) ;
#9237=ORIENTED_EDGE ( 'NONE', *, *, #4635, .T. ) ;
#9259=ORIENTED_EDGE ( 'NONE', *, *, #214, .F. ) ;
#9264=DIRECTION ( 'NONE',  ( 0.000000000000000000, 0.000000000000000000, 1.000000000000000000 ) ) ;
#9275=ORIENTED_EDGE ( 'NONE', *, *, #9374, .F. ) ;
#9305=AXIS2_PLACEMENT_3D ( 'NONE', #11903, #717, #2761 ) ;
#9307=ORIENTED_EDGE ( 'NONE', *, *, #4122, .F. ) ;
#9327=VERTEX_POINT ( 'NONE', #9890 ) ;
#9360=DIRECTION ( 'NONE',  ( 1.000000000000000000, 0.000000000000000000, 0.000000000000000000 ) ) ;
#9374=EDGE_CURVE ( 'NONE', #5809, #9809, #8353, .T. ) ;
#9384=DIRECTION ( 'NONE',  ( 0.03100775193798453039, -0.9995191440486532741, 0.000000000000000000 ) ) ;
#9411=ORIENTED_EDGE ( 'NONE', *, *, #11395, .F. ) ;
#9429=CARTESIAN_POINT ( 'NONE',  ( -0.1038759689922479496, -3.348389132562988646, -0.8000000000000000444 ) ) ;
#9432=ORIENTED_EDGE ( 'NONE', *, *, #11576, .F. ) ;
#9446=CIRCLE ( 'NONE', #11107, 4.338286831716297698 ) ;
#9454=AXIS2_PLACEMENT_3D ( 'NONE', #9078, #106, #12817 ) ;
#9459=CARTESIAN_POINT ( 'NONE',  ( -1.625004804578467077, -6.241943558307533557, -0.8000000000000000444 ) ) ;
#9472=( GEOMETRIC_REPRESENTATION_CONTEXT ( 3 ) GLOBAL_UNCERTAINTY_ASSIGNED_CONTEXT ( ( #1193 ) ) GLOBAL_UNIT_ASSIGNED_CONTEXT ( ( #9138, #11954, #31 ) ) REPRESENTATION_CONTEXT ( 'NONE', 'WORKASPACE' ) );
#9474=EDGE_LOOP ( 'NONE', ( #2087, #4424, #5098, #11071 ) ) ;
#9478=DIRECTION ( 'NONE',  ( 1.000000000000000000, 0.000000000000000000, 0.000000000000000000 ) ) ;
#9498=ORIENTED_EDGE ( 'NONE', *, *, #8313, .T. ) ;
#9501=PRODUCT_DEFINITION_SHAPE ( 'NONE', 'NONE',  #12586 ) ;
#9511=DIRECTION ( 'NONE',  ( 0.000000000000000000, 0.000000000000000000, 1.000000000000000000 ) ) ;
#9537=VERTEX_POINT ( 'NONE', #5499 ) ;
#9563=ORIENTED_EDGE ( 'NONE', *, *, #3846, .T. ) ;
#9579=DIRECTION ( 'NONE',  ( 0.1305261922200528224, -0.9914448613738103822, 0.000000000000000000 ) ) ;
#9591=CIRCLE ( 'NONE', #11673, 6.450000000000001066 ) ;
#9614=EDGE_LOOP ( 'NONE', ( #2570, #1704, #5288, #6502 ) ) ;
#9643=EDGE_CURVE ( 'NONE', #3461, #6695, #2891, .T. ) ;
#9652=EDGE_CURVE ( 'NONE', #6795, #11778, #817, .T. ) ;
#9663=EDGE_LOOP ( 'NONE', ( #7714, #5964, #9027, #6713 ) ) ;
#9706=ORIENTED_EDGE ( 'NONE', *, *, #3741, .F. ) ;
#9714=EDGE_CURVE ( 'NONE', #870, #9327, #7984, .T. ) ;
#9732=LINE ( 'NONE', #3358, #3969 ) ;
#9741=CYLINDRICAL_SURFACE ( 'NONE', #2227, 3.350000000000000089 ) ;
#9752=ORIENTED_EDGE ( 'NONE', *, *, #4943, .T. ) ;
#9761=VECTOR ( 'NONE', #5009, 999.9999999999998863 ) ;
#9769=AXIS2_PLACEMENT_3D ( 'NONE', #2854, #4938, #12853 ) ;
#9793=CARTESIAN_POINT ( 'NONE',  ( 0.1999999999999965694, -6.446898479113814417, -0.8000000000000000444 ) ) ;
#9806=EDGE_LOOP ( 'NONE', ( #3212, #12281, #1290, #7859 ) ) ;
#9809=VERTEX_POINT ( 'NONE', #7906 ) ;
#9821=CIRCLE ( 'NONE', #6049, 4.338286831716297698 ) ;
#9837=ORIENTED_EDGE ( 'NONE', *, *, #7034, .T. ) ;
#9839=AXIS2_PLACEMENT_3D ( 'NONE', #7943, #4866, #8853 ) ;
#9890=CARTESIAN_POINT ( 'NONE',  ( 1.599999999999999867, -4.873461295629625489, 0.000000000000000000 ) ) ;
#9926=VERTEX_POINT ( 'NONE', #7772 ) ;
#9928=( NAMED_UNIT ( * ) PLANE_ANGLE_UNIT ( ) SI_UNIT ( $, .RADIAN. ) );
#9932=VECTOR ( 'NONE', #3315, 1000.000000000000000 ) ;
#9946=EDGE_CURVE ( 'NONE', #1140, #5809, #9821, .T. ) ;
#9987=CARTESIAN_POINT ( 'NONE',  ( -1.625004804578467077, -6.241943558307533557, 0.000000000000000000 ) ) ;
#10019=ORIENTED_EDGE ( 'NONE', *, *, #5002, .F. ) ;
#10038=CARTESIAN_POINT ( 'NONE',  ( 0.000000000000000000, 0.4117131682837005258, -0.8000000000000000444 ) ) ;
#10041=DIRECTION ( 'NONE',  ( 0.000000000000000000, 0.000000000000000000, 1.000000000000000000 ) ) ;
#10048=DIRECTION ( 'NONE',  ( 1.000000000000000000, 0.000000000000000000, 0.000000000000000000 ) ) ;
#10050=VERTEX_POINT ( 'NONE', #7113 ) ;
#10065=PRODUCT_CONTEXT ( 'NONE', #6833, 'mechanical' ) ;
#10073=CYLINDRICAL_SURFACE ( 'NONE', #3293, 0.5999999999999999778 ) ;
#10075=CIRCLE ( 'NONE', #9454, 6.450000000000001066 ) ;
#10094=DIRECTION ( 'NONE',  ( 0.000000000000000000, 0.000000000000000000, 1.000000000000000000 ) ) ;
#10095=STYLED_ITEM ( 'NONE', ( #2150 ), #12938 ) ;
#10123=DIRECTION ( 'NONE',  ( -1.000000000000000000, -0.000000000000000000, -0.000000000000000000 ) ) ;
#10142=FACE_OUTER_BOUND ( 'NONE', #9207, .T. ) ;
#10155=DIRECTION ( 'NONE',  ( 1.000000000000000000, 0.000000000000000000, 0.000000000000000000 ) ) ;
#10157=DIRECTION ( 'NONE',  ( -0.000000000000000000, -0.000000000000000000, -1.000000000000000000 ) ) ;
#10158=EDGE_CURVE ( 'NONE', #7369, #9537, #10382, .T. ) ;
#10163=CARTESIAN_POINT ( 'NONE',  ( 0.000000000000000000, 0.000000000000000000, -0.8000000000000000444 ) ) ;
#10164=CARTESIAN_POINT ( 'NONE',  ( -0.1325741768533960085, -4.273461295629625845, -0.8000000000000000444 ) ) ;
#10186=AXIS2_PLACEMENT_3D ( 'NONE', #3043, #74, #3177 ) ;
#10224=CARTESIAN_POINT ( 'NONE',  ( 0.000000000000000000, 0.000000000000000000, -0.8000000000000000444 ) ) ;
#10226=CIRCLE ( 'NONE', #4795, 2.396199811936270407 ) ;
#10234=FACE_OUTER_BOUND ( 'NONE', #1556, .T. ) ;
#10240=ADVANCED_FACE ( 'NONE', ( #10509 ), #5401, .T. ) ;
#10245=CARTESIAN_POINT ( 'NONE',  ( 4.763019983628629994, -4.349268977144817860, -0.8000000000000000444 ) ) ;
#10251=ORIENTED_EDGE ( 'NONE', *, *, #3895, .T. ) ;
#10267=CIRCLE ( 'NONE', #853, 4.338286831716297698 ) ;
#10281=EDGE_LOOP ( 'NONE', ( #560, #9706, #5084, #11040 ) ) ;
#10292=CARTESIAN_POINT ( 'NONE',  ( 4.338286831716297698, 0.4117131682837005258, 0.000000000000000000 ) ) ;
#10293=VECTOR ( 'NONE', #7639, 999.9999999999998863 ) ;
#10297=PLANE ( 'NONE',  #3477 ) ;
#10317=CIRCLE ( 'NONE', #2593, 0.7499999999999997780 ) ;
#10333=CARTESIAN_POINT ( 'NONE',  ( -1.436050757534458100, -5.516136167806656943, -0.8000000000000000444 ) ) ;
#10344=CARTESIAN_POINT ( 'NONE',  ( 0.1999999999999965694, -6.446898479113814417, 0.000000000000000000 ) ) ;
#10349=VECTOR ( 'NONE', #9134, 1000.000000000000000 ) ;
#10355=ORIENTED_EDGE ( 'NONE', *, *, #5724, .T. ) ;
#10376=CYLINDRICAL_SURFACE ( 'NONE', #11662, 2.396199811936269963 ) ;
#10382=LINE ( 'NONE', #555, #5428 ) ;
#10438=EDGE_CURVE ( 'NONE', #5034, #85, #1266, .T. ) ;
#10472=ORIENTED_EDGE ( 'NONE', *, *, #12514, .T. ) ;
#10479=ORIENTED_EDGE ( 'NONE', *, *, #9714, .F. ) ;
#10491=FACE_OUTER_BOUND ( 'NONE', #1650, .T. ) ;
#10503=CARTESIAN_POINT ( 'NONE',  ( -3.350000000000000089, 4.102566777143633281E-16, -0.8000000000000000444 ) ) ;
#10509=FACE_OUTER_BOUND ( 'NONE', #6542, .T. ) ;
#10527=DIRECTION ( 'NONE',  ( -0.000000000000000000, -0.000000000000000000, -1.000000000000000000 ) ) ;
#10533=VERTEX_POINT ( 'NONE', #8991 ) ;
#10546=EDGE_CURVE ( 'NONE', #169, #5034, #2923, .T. ) ;
#10557=CARTESIAN_POINT ( 'NONE',  ( -0.1038759689922479496, -3.348389132562988646, -0.8000000000000000444 ) ) ;
#10576=EDGE_CURVE ( 'NONE', #10533, #6247, #7889, .T. ) ;
#10629=ORIENTED_EDGE ( 'NONE', *, *, #8366, .F. ) ;
#10657=LINE ( 'NONE', #1760, #3265 ) ;
#10659=DIRECTION ( 'NONE',  ( 0.000000000000000000, 0.000000000000000000, 1.000000000000000000 ) ) ;
#10661=EDGE_CURVE ( 'NONE', #3461, #1892, #11281, .T. ) ;
#10668=FACE_OUTER_BOUND ( 'NONE', #5829, .T. ) ;
#10669=ORIENTED_EDGE ( 'NONE', *, *, #10438, .F. ) ;
#10675=EDGE_LOOP ( 'NONE', ( #1011, #10877, #11201, #12854 ) ) ;
#10705=DIRECTION ( 'NONE',  ( 0.000000000000000000, 0.000000000000000000, 1.000000000000000000 ) ) ;
#10726=ORIENTED_EDGE ( 'NONE', *, *, #812, .F. ) ;
#10737=DIRECTION ( 'NONE',  ( 0.000000000000000000, 0.000000000000000000, 1.000000000000000000 ) ) ;
#10749=VECTOR ( 'NONE', #6105, 1000.000000000000000 ) ;
#10760=AXIS2_PLACEMENT_3D ( 'NONE', #4609, #9511, #6429 ) ;
#10775=VECTOR ( 'NONE', #9579, 999.9999999999998863 ) ;
#10778=CARTESIAN_POINT ( 'NONE',  ( -0.9999999999999997780, -4.273461295629625845, -0.8000000000000000444 ) ) ;
#10798=ORIENTED_EDGE ( 'NONE', *, *, #10438, .T. ) ;
#10799=DIRECTION ( 'NONE',  ( 1.000000000000000000, -0.000000000000000000, -0.000000000000000000 ) ) ;
#10800=ORIENTED_EDGE ( 'NONE', *, *, #12372, .F. ) ;
#10813=AXIS2_PLACEMENT_3D ( 'NONE', #8413, #3448, #2529 ) ;
#10835=EDGE_CURVE ( 'NONE', #7668, #9926, #7807, .T. ) ;
#10877=ORIENTED_EDGE ( 'NONE', *, *, #6150, .F. ) ;
#10892=ORIENTED_EDGE ( 'NONE', *, *, #10987, .F. ) ;
#10902=DIRECTION ( 'NONE',  ( 0.000000000000000000, 0.000000000000000000, 1.000000000000000000 ) ) ;
#10906=MECHANICAL_DESIGN_GEOMETRIC_PRESENTATION_REPRESENTATION('',(#1930),#6727);
#10945=AXIS2_PLACEMENT_3D ( 'NONE', #10038, #6303, #1069 ) ;
#10954=EDGE_LOOP ( 'NONE', ( #10629, #12301, #6183, #4437 ) ) ;
#10959=EDGE_CURVE ( 'NONE', #3461, #2471, #3036, .T. ) ;
#10987=EDGE_CURVE ( 'NONE', #2471, #11510, #3958, .T. ) ;
#10994=ORIENTED_EDGE ( 'NONE', *, *, #10158, .F. ) ;
#11016=DIRECTION ( 'NONE',  ( 0.000000000000000000, 0.000000000000000000, 1.000000000000000000 ) ) ;
#11017=DIRECTION ( 'NONE',  ( 0.000000000000000000, 0.000000000000000000, 1.000000000000000000 ) ) ;
#11019=AXIS2_PLACEMENT_3D ( 'NONE', #2384, #5444, #5378 ) ;
#11036=ORIENTED_EDGE ( 'NONE', *, *, #1642, .F. ) ;
#11037=AXIS2_PLACEMENT_3D ( 'NONE', #12455, #3433, #599 ) ;
#11039=CARTESIAN_POINT ( 'NONE',  ( -3.068288344391240763, -2.655262421758692426, -0.8000000000000000444 ) ) ;
#11040=ORIENTED_EDGE ( 'NONE', *, *, #4122, .T. ) ;
#11055=CARTESIAN_POINT ( 'NONE',  ( -4.763019983628629994, -4.349268977144818749, -0.8000000000000000444 ) ) ;
#11060=ADVANCED_FACE ( 'NONE', ( #8006 ), #863, .T. ) ;
#11071=ORIENTED_EDGE ( 'NONE', *, *, #7158, .F. ) ;
#11074=DIRECTION ( 'NONE',  ( -0.9914448613738103822, -0.1305261922200528224, 0.000000000000000000 ) ) ;
#11079=CYLINDRICAL_SURFACE ( 'NONE', #10945, 4.338286831716297698 ) ;
#11096=SURFACE_STYLE_FILL_AREA ( #2220 ) ;
#11107=AXIS2_PLACEMENT_3D ( 'NONE', #3483, #11315, #9360 ) ;
#11120=DIRECTION ( 'NONE',  ( -0.000000000000000000, -0.000000000000000000, -1.000000000000000000 ) ) ;
#11140=LINE ( 'NONE', #6367, #10749 ) ;
#11187=ORIENTED_EDGE ( 'NONE', *, *, #7674, .F. ) ;
#11191=DIRECTION ( 'NONE',  ( 1.000000000000000000, 0.000000000000000000, 0.000000000000000000 ) ) ;
#11194=CIRCLE ( 'NONE', #7230, 0.5999999999999999778 ) ;
#11201=ORIENTED_EDGE ( 'NONE', *, *, #4981, .T. ) ;
#11202=EDGE_CURVE ( 'NONE', #6201, #7668, #634, .T. ) ;
#11214=VECTOR ( 'NONE', #11914, 1000.000000000000000 ) ;
#11217=CARTESIAN_POINT ( 'NONE',  ( 0.000000000000000000, 0.4117131682837005258, -0.8000000000000000444 ) ) ;
#11221=VERTEX_POINT ( 'NONE', #1260 ) ;
#11253=DIRECTION ( 'NONE',  ( 0.000000000000000000, -1.000000000000000000, -0.000000000000000000 ) ) ;
#11260=DIRECTION ( 'NONE',  ( -0.000000000000000000, -0.000000000000000000, -1.000000000000000000 ) ) ;
#11274=EDGE_CURVE ( 'NONE', #9327, #1939, #7121, .T. ) ;
#11280=CARTESIAN_POINT ( 'NONE',  ( 2.179634403564814971, -5.614030811971695734, -0.8000000000000000444 ) ) ;
#11281=LINE ( 'NONE', #11342, #8985 ) ;
#11294=CARTESIAN_POINT ( 'NONE',  ( 0.1038759689922479496, -3.348389132562988646, -0.8000000000000000444 ) ) ;
#11311=AXIS2_PLACEMENT_3D ( 'NONE', #12397, #5523, #11413 ) ;
#11315=DIRECTION ( 'NONE',  ( 0.000000000000000000, 0.000000000000000000, 1.000000000000000000 ) ) ;
#11316=CARTESIAN_POINT ( 'NONE',  ( -4.338286831716297698, 0.4117131682837010809, 0.000000000000000000 ) ) ;
#11342=CARTESIAN_POINT ( 'NONE',  ( 0.1038759689922479496, -3.348389132562988646, -0.8000000000000000444 ) ) ;
#11359=EDGE_CURVE ( 'NONE', #6548, #4634, #5705, .T. ) ;
#11365=LINE ( 'NONE', #8106, #3200 ) ;
#11395=EDGE_CURVE ( 'NONE', #4659, #6247, #10267, .T. ) ;
#11400=CYLINDRICAL_SURFACE ( 'NONE', #7901, 6.450000000000001066 ) ;
#11402=PLANE ( 'NONE',  #3746 ) ;
#11405=FACE_OUTER_BOUND ( 'NONE', #3899, .T. ) ;
#11413=DIRECTION ( 'NONE',  ( 0.03100775193798452692, 0.9995191440486532741, 0.000000000000000000 ) ) ;
#11435=PLANE ( 'NONE',  #8437 ) ;
#11439=CARTESIAN_POINT ( 'NONE',  ( 2.179634403564814971, -5.614030811971695734, -0.8000000000000000444 ) ) ;
#11445=CYLINDRICAL_SURFACE ( 'NONE', #7974, 4.338286831716297698 ) ;
#11447=VECTOR ( 'NONE', #1377, 1000.000000000000000 ) ;
#11467=CARTESIAN_POINT ( 'NONE',  ( 2.387319993259524598, -4.036502139894371233, -0.8000000000000000444 ) ) ;
#11468=DIRECTION ( 'NONE',  ( 0.03100775193798453039, 0.9995191440486532741, -0.000000000000000000 ) ) ;
#11471=DIRECTION ( 'NONE',  ( 1.000000000000000000, 0.000000000000000000, 0.000000000000000000 ) ) ;
#11490=ORIENTED_EDGE ( 'NONE', *, *, #3056, .F. ) ;
#11497=ORIENTED_EDGE ( 'NONE', *, *, #12347, .T. ) ;
#11510=VERTEX_POINT ( 'NONE', #11849 ) ;
#11528=LINE ( 'NONE', #3626, #963 ) ;
#11534=CARTESIAN_POINT ( 'NONE',  ( -0.1038759689922479496, -3.348389132562988646, -0.8000000000000000444 ) ) ;
#11567=CARTESIAN_POINT ( 'NONE',  ( -0.1038759689922479496, -3.348389132562988646, 0.000000000000000000 ) ) ;
#11575=ORIENTED_EDGE ( 'NONE', *, *, #9946, .F. ) ;
#11576=EDGE_CURVE ( 'NONE', #11510, #9327, #11725, .T. ) ;
#11610=DIRECTION ( 'NONE',  ( -0.000000000000000000, -0.000000000000000000, 1.000000000000000000 ) ) ;
#11625=ORIENTED_EDGE ( 'NONE', *, *, #3895, .F. ) ;
#11644=ORIENTED_EDGE ( 'NONE', *, *, #1100, .F. ) ;
#11650=CARTESIAN_POINT ( 'NONE',  ( -0.9999999999999997780, -4.273461295629625845, -0.8000000000000000444 ) ) ;
#11662=AXIS2_PLACEMENT_3D ( 'NONE', #10245, #5270, #12078 ) ;
#11673=AXIS2_PLACEMENT_3D ( 'NONE', #10163, #10094, #5124 ) ;
#11684=CARTESIAN_POINT ( 'NONE',  ( -1.436050757534458100, -5.516136167806656943, 0.000000000000000000 ) ) ;
#11690=CARTESIAN_POINT ( 'NONE',  ( -0.1038759689922479496, -3.348389132562988646, -0.8000000000000000444 ) ) ;
#11717=VECTOR ( 'NONE', #6954, 1000.000000000000000 ) ;
#11720=DIRECTION ( 'NONE',  ( 0.000000000000000000, 0.000000000000000000, 1.000000000000000000 ) ) ;
#11725=CIRCLE ( 'NONE', #6499, 0.5999999999999998668 ) ;
#11729=DIRECTION ( 'NONE',  ( 1.000000000000000000, 0.000000000000000000, 0.000000000000000000 ) ) ;
#11735=EDGE_CURVE ( 'NONE', #1744, #85, #1703, .T. ) ;
#11741=LINE ( 'NONE', #12857, #2401 ) ;
#11759=ADVANCED_FACE ( 'NONE', ( #12695 ), #11445, .T. ) ;
#11763=CARTESIAN_POINT ( 'NONE',  ( 0.000000000000000000, 0.4117131682837005258, -0.8000000000000000444 ) ) ;
#11778=VERTEX_POINT ( 'NONE', #7718 ) ;
#11787=CARTESIAN_POINT ( 'NONE',  ( 3.068288344391240763, -2.655262421758693314, -0.8000000000000000444 ) ) ;
#11798=CARTESIAN_POINT ( 'NONE',  ( 0.000000000000000000, 0.000000000000000000, 0.000000000000000000 ) ) ;
#11814=CARTESIAN_POINT ( 'NONE',  ( 1.000000000000000000, -4.273461295629625845, 0.000000000000000000 ) ) ;
#11820=CARTESIAN_POINT ( 'NONE',  ( 3.068288344391240763, -2.655262421758693314, 0.000000000000000000 ) ) ;
#11849=CARTESIAN_POINT ( 'NONE',  ( 1.000000000000000000, -5.473461295629626022, 0.000000000000000000 ) ) ;
#11885=VECTOR ( 'NONE', #8273, 1000.000000000000000 ) ;
#11886=CARTESIAN_POINT ( 'NONE',  ( 0.1038759689922479496, -3.348389132562988646, -0.8000000000000000444 ) ) ;
#11903=CARTESIAN_POINT ( 'NONE',  ( 0.000000000000000000, 0.000000000000000000, 0.000000000000000000 ) ) ;
#11914=DIRECTION ( 'NONE',  ( -1.000000000000000000, -0.000000000000000000, -0.000000000000000000 ) ) ;
#11931=ORIENTED_EDGE ( 'NONE', *, *, #3298, .T. ) ;
#11933=CARTESIAN_POINT ( 'NONE',  ( -2.387319993259524598, -4.036502139894371233, 0.000000000000000000 ) ) ;
#11949=CARTESIAN_POINT ( 'NONE',  ( 1.625004804578465745, -6.241943558307532669, -0.8000000000000000444 ) ) ;
#11954=( NAMED_UNIT ( * ) PLANE_ANGLE_UNIT ( ) SI_UNIT ( $, .RADIAN. ) );
#11968=CARTESIAN_POINT ( 'NONE',  ( 1.599999999999999867, -4.873461295629625489, -0.8000000000000000444 ) ) ;
#11979=ADVANCED_FACE ( 'NONE', ( #8412 ), #2224, .T. ) ;
#11996=DIRECTION ( 'NONE',  ( 0.000000000000000000, 0.000000000000000000, 1.000000000000000000 ) ) ;
#12008=VECTOR ( 'NONE', #5432, 1000.000000000000114 ) ;
#12022=ORIENTED_EDGE ( 'NONE', *, *, #10959, .T. ) ;
#12053=DIRECTION ( 'NONE',  ( -0.000000000000000000, -0.000000000000000000, -1.000000000000000000 ) ) ;
#12058=DIRECTION ( 'NONE',  ( 1.000000000000000000, -0.000000000000000000, -0.000000000000000000 ) ) ;
#12065=PLANE ( 'NONE',  #8553 ) ;
#12069=DIRECTION ( 'NONE',  ( 0.9995191440486532741, -0.03100775193798452692, 0.000000000000000000 ) ) ;
#12078=DIRECTION ( 'NONE',  ( 1.000000000000000000, 0.000000000000000000, 0.000000000000000000 ) ) ;
#12119=CARTESIAN_POINT ( 'NONE',  ( 0.000000000000000000, 0.000000000000000000, -0.8000000000000000444 ) ) ;
#12155=ORIENTED_EDGE ( 'NONE', *, *, #1444, .T. ) ;
#12156=MANIFOLD_SOLID_BREP ( 'Notch', #1111 ) ;
#12171=CARTESIAN_POINT ( 'NONE',  ( 1.000000000000000000, -4.273461295629625845, -0.8000000000000000444 ) ) ;
#12177=DIRECTION ( 'NONE',  ( 0.000000000000000000, 0.000000000000000000, 1.000000000000000000 ) ) ;
#12209=PRODUCT ( 'circlip for shafts normal_din_Circlip DIN 471 - 7 x 0.8', 'circlip for shafts normal_din_Circlip DIN 471 - 7 x 0.8', '', ( #10065 ) ) ;
#12216=AXIS2_PLACEMENT_3D ( 'NONE', #11763, #2811, #3669 ) ;
#12217=LINE ( 'NONE', #1151, #10349 ) ;
#12221=FILL_AREA_STYLE_COLOUR ( '', #2169 ) ;
#12223=ORIENTED_EDGE ( 'NONE', *, *, #4725, .T. ) ;
#12236=ORIENTED_EDGE ( 'NONE', *, *, #10835, .T. ) ;
#12242=AXIS2_PLACEMENT_3D ( 'NONE', #4173, #9264, #10048 ) ;
#12247=CARTESIAN_POINT ( 'NONE',  ( -4.763019983628629994, -4.349268977144818749, 0.000000000000000000 ) ) ;
#12253=ORIENTED_EDGE ( 'NONE', *, *, #10546, .T. ) ;
#12263=DIRECTION ( 'NONE',  ( 1.000000000000000000, -0.000000000000000000, -0.000000000000000000 ) ) ;
#12281=ORIENTED_EDGE ( 'NONE', *, *, #6543, .F. ) ;
#12301=ORIENTED_EDGE ( 'NONE', *, *, #7427, .F. ) ;
#12315=ORIENTED_EDGE ( 'NONE', *, *, #2114, .F. ) ;
#12324=DIRECTION ( 'NONE',  ( 1.000000000000000000, 0.000000000000000000, 0.000000000000000000 ) ) ;
#12346=CARTESIAN_POINT ( 'NONE',  ( -0.9999999999999997780, -4.273461295629625845, 0.000000000000000000 ) ) ;
#12347=EDGE_CURVE ( 'NONE', #11778, #10533, #9446, .T. ) ;
#12362=ADVANCED_FACE ( 'NONE', ( #10142 ), #7269, .F. ) ;
#12369=CARTESIAN_POINT ( 'NONE',  ( 1.000000000000000000, -5.473461295629626022, -0.8000000000000000444 ) ) ;
#12372=EDGE_CURVE ( 'NONE', #1569, #10050, #7148, .T. ) ;
#12384=DIRECTION ( 'NONE',  ( 0.000000000000000000, 0.000000000000000000, 1.000000000000000000 ) ) ;
#12397=CARTESIAN_POINT ( 'NONE',  ( -0.1038759689922479496, -3.348389132562988646, -0.8000000000000000444 ) ) ;
#12407=DIRECTION ( 'NONE',  ( 0.03100775193798452692, -0.9995191440486532741, 0.000000000000000000 ) ) ;
#12422=FACE_OUTER_BOUND ( 'NONE', #6475, .T. ) ;
#12434=DIRECTION ( 'NONE',  ( 0.000000000000000000, 0.000000000000000000, 1.000000000000000000 ) ) ;
#12455=CARTESIAN_POINT ( 'NONE',  ( 0.000000000000000000, 0.000000000000000000, -0.8000000000000000444 ) ) ;
#12476=ORIENTED_EDGE ( 'NONE', *, *, #12347, .F. ) ;
#12477=CARTESIAN_POINT ( 'NONE',  ( 1.436050757534458100, -5.516136167806656943, 0.000000000000000000 ) ) ;
#12490=ORIENTED_EDGE ( 'NONE', *, *, #8366, .T. ) ;
#12500=DIRECTION ( 'NONE',  ( 0.000000000000000000, 0.000000000000000000, -1.000000000000000000 ) ) ;
#12514=EDGE_CURVE ( 'NONE', #5455, #9206, #10075, .T. ) ;
#12521=CYLINDRICAL_SURFACE ( 'NONE', #11037, 6.450000000000001066 ) ;
#12524=EDGE_CURVE ( 'NONE', #12851, #9926, #2368, .T. ) ;
#12527=AXIS2_PLACEMENT_3D ( 'NONE', #2764, #3874, #5825 ) ;
#12560=CARTESIAN_POINT ( 'NONE',  ( 0.000000000000000000, 0.000000000000000000, -0.8000000000000000444 ) ) ;
#12563=CARTESIAN_POINT ( 'NONE',  ( 0.000000000000000000, 0.000000000000000000, 0.000000000000000000 ) ) ;
#12575=VERTEX_POINT ( 'NONE', #1895 ) ;
#12586=PRODUCT_DEFINITION ( 'UNKNOWN', '', #7401, #5412 ) ;
#12587=DIRECTION ( 'NONE',  ( 0.000000000000000000, 0.000000000000000000, 1.000000000000000000 ) ) ;
#12626=CARTESIAN_POINT ( 'NONE',  ( 0.000000000000000000, 0.000000000000000000, -0.8000000000000000444 ) ) ;
#12630=ORIENTED_EDGE ( 'NONE', *, *, #10987, .T. ) ;
#12676=EDGE_CURVE ( 'NONE', #1939, #8099, #11365, .T. ) ;
#12684=DIRECTION ( 'NONE',  ( 1.000000000000000000, 0.000000000000000000, -0.000000000000000000 ) ) ;
#12695=FACE_OUTER_BOUND ( 'NONE', #6915, .T. ) ;
#12707=VERTEX_POINT ( 'NONE', #8369 ) ;
#12751=LINE ( 'NONE', #6788, #3456 ) ;
#12758=VECTOR ( 'NONE', #10041, 1000.000000000000000 ) ;
#12761=EDGE_CURVE ( 'NONE', #1154, #6795, #2482, .T. ) ;
#12768=AXIS2_PLACEMENT_3D ( 'NONE', #10224, #10157, #5441 ) ;
#12790=AXIS2_PLACEMENT_3D ( 'NONE', #12369, #11253, #3223 ) ;
#12802=LINE ( 'NONE', #9793, #589 ) ;
#12809=CARTESIAN_POINT ( 'NONE',  ( 0.000000000000000000, 0.4117131682837005258, -0.8000000000000000444 ) ) ;
#12812=FACE_OUTER_BOUND ( 'NONE', #4434, .T. ) ;
#12817=DIRECTION ( 'NONE',  ( 1.000000000000000000, 0.000000000000000000, 0.000000000000000000 ) ) ;
#12819=CARTESIAN_POINT ( 'NONE',  ( -0.2000000000000000111, -6.446898479113814417, -0.8000000000000000444 ) ) ;
#12826=ORIENTED_EDGE ( 'NONE', *, *, #5002, .T. ) ;
#12840=CIRCLE ( 'NONE', #1558, 3.350000000000000089 ) ;
#12851=VERTEX_POINT ( 'NONE', #3467 ) ;
#12853=DIRECTION ( 'NONE',  ( 1.000000000000000000, 0.000000000000000000, 0.000000000000000000 ) ) ;
#12854=ORIENTED_EDGE ( 'NONE', *, *, #6371, .T. ) ;
#12857=CARTESIAN_POINT ( 'NONE',  ( 1.000000000000000000, -4.273461295629625845, -0.8000000000000000444 ) ) ;
#12862=CIRCLE ( 'NONE', #12242, 0.5999999999999998668 ) ;
#12881=ORIENTED_EDGE ( 'NONE', *, *, #7105, .F. ) ;
#12883=CARTESIAN_POINT ( 'NONE',  ( 0.000000000000000000, 0.000000000000000000, -0.8000000000000000444 ) ) ;
#12937=ORIENTED_EDGE ( 'NONE', *, *, #1279, .F. ) ;
#12938=ADVANCED_BREP_SHAPE_REPRESENTATION ( '', ( #12156, #5704 ), #1107 ) ;
#12996=COLOUR_RGB('Grey',0.48,0.52,0.57);
#12997=FILL_AREA_STYLE_COLOUR('',#12996);
#12998=FILL_AREA_STYLE('',(#12997));
#12999=SURFACE_STYLE_FILL_AREA(#12998);
#13000=SURFACE_SIDE_STYLE('',(#12999));
#13001=SURFACE_STYLE_USAGE(.BOTH.,#13000);
#13002=PRESENTATION_STYLE_ASSIGNMENT((#13001));
ENDSEC;
END-ISO-10303-21;
